ISO-10303-21;
HEADER;
FILE_DESCRIPTION (('STEP AP214'),
    '1' );
FILE_NAME ('isolation 510.step',
    '2026-10-05T20:10:51',
    ( '' ),
    ( '' ),
    'SwSTEP 2.0',
    'SolidWorks 2020',
    '' );
FILE_SCHEMA (( 'AUTOMOTIVE_DESIGN' ));
ENDSEC;

DATA;
#1=ORIENTED_EDGE ( 'NONE', *, *, #97562, .T. ) ;
#106=VERTEX_POINT ( 'NONE', #173218 ) ;
#675=LINE ( 'NONE', #198886, #145063 ) ;
#677=DIRECTION ( 'NONE',  ( 0.000000000000000000, 1.000000000000000000, 0.000000000000000000 ) ) ;
#1087=CARTESIAN_POINT ( 'NONE',  ( 0.000000000000000000, 4.000000000000003553, 0.000000000000000000 ) ) ;
#1174=AXIS2_PLACEMENT_3D ( 'NONE', #114767, #111570, #194880 ) ;
#1270=ORIENTED_EDGE ( 'NONE', *, *, #25737, .T. ) ;
#1764=AXIS2_PLACEMENT_3D ( 'NONE', #37629, #151395, #118947 ) ;
#1852=EDGE_CURVE ( 'NONE', #197886, #149924, #212986, .T. ) ;
#1866=EDGE_CURVE ( 'NONE', #136049, #106, #60036, .T. ) ;
#2112=DIRECTION ( 'NONE',  ( 0.000000000000000000, 1.000000000000000000, 0.000000000000000000 ) ) ;
#2848=LINE ( 'NONE', #201050, #103212 ) ;
#2876=DIRECTION ( 'NONE',  ( 0.000000000000000000, -1.000000000000000000, 0.000000000000000000 ) ) ;
#3054=LINE ( 'NONE', #51848, #199489 ) ;
#3245=CARTESIAN_POINT ( 'NONE',  ( 0.000000000000000000, 2.099999999999997868, 0.000000000000000000 ) ) ;
#3487=COLOUR_RGB ( '', 0.31764706, 0.68627451, 0.89019608) ;
#3609=DIRECTION ( 'NONE',  ( -1.000000000000000000, 0.000000000000000000, -5.551115123125765446E-17 ) ) ;
#3724=AXIS2_PLACEMENT_3D ( 'NONE', #115620, #133988, #166450 ) ;
#3765=ORIENTED_EDGE ( 'NONE', *, *, #142604, .T. ) ;
#3781=DIRECTION ( 'NONE',  ( 5.551115123125766062E-17, 0.000000000000000000, -1.000000000000000000 ) ) ;
#3946=FACE_BOUND ( 'NONE', #188223, .T. ) ;
#4335=AXIS2_PLACEMENT_3D ( 'NONE', #96713, #117247, #46885 ) ;
#4463=LINE ( 'NONE', #184302, #7915 ) ;
#4493=ORIENTED_EDGE ( 'NONE', *, *, #181245, .T. ) ;
#4619=FACE_BOUND ( 'NONE', #32942, .T. ) ;
#5008=DIRECTION ( 'NONE',  ( 0.3085202182251676195, 0.000000000000000000, -0.9512177852344304574 ) ) ;
#5049=DIRECTION ( 'NONE',  ( -5.551115123125766062E-17, 0.000000000000000000, 1.000000000000000000 ) ) ;
#5311=CARTESIAN_POINT ( 'NONE',  ( 1.124100812432970948E-16, 2.999999999999975131, -2.025000000000006573 ) ) ;
#5551=DIRECTION ( 'NONE',  ( 0.000000000000000000, 1.000000000000000000, 0.000000000000000000 ) ) ;
#5680=AXIS2_PLACEMENT_3D ( 'NONE', #105900, #24587, #126455 ) ;
#5806=FACE_BOUND ( 'NONE', #190877, .T. ) ;
#6058=CARTESIAN_POINT ( 'NONE',  ( 0.000000000000000000, 3.500000000000003109, 0.000000000000000000 ) ) ;
#6470=CYLINDRICAL_SURFACE ( 'NONE', #132658, 2.025000000000006573 ) ;
#6484=DIRECTION ( 'NONE',  ( 0.000000000000000000, -1.000000000000000000, 0.000000000000000000 ) ) ;
#6645=DIRECTION ( 'NONE',  ( 1.000000000000000000, -0.000000000000000000, 1.779758311459929752E-16 ) ) ;
#6947=FACE_OUTER_BOUND ( 'NONE', #134636, .T. ) ;
#7300=UNCERTAINTY_MEASURE_WITH_UNIT (LENGTH_MEASURE( 1.000000000000000082E-05 ), #207618, 'distance_accuracy_value', 'NONE');
#7345=DIRECTION ( 'NONE',  ( 0.000000000000000000, 1.000000000000000000, 0.000000000000000000 ) ) ;
#7497=DIRECTION ( 'NONE',  ( 5.551115123125765446E-17, 0.000000000000000000, -1.000000000000000000 ) ) ;
#7915=VECTOR ( 'NONE', #52190, 1000.000000000000000 ) ;
#7939=ORIENTED_EDGE ( 'NONE', *, *, #181170, .T. ) ;
#8511=CARTESIAN_POINT ( 'NONE',  ( 0.000000000000000000, 3.599999999999999201, 0.000000000000000000 ) ) ;
#8603=TOROIDAL_SURFACE ( 'NONE', #129777, 2.349999999999999645, 0.1000000000000000056 ) ;
#8863=ORIENTED_EDGE ( 'NONE', *, *, #42520, .F. ) ;
#9073=VERTEX_POINT ( 'NONE', #124895 ) ;
#9515=DIRECTION ( 'NONE',  ( 5.551115123125764829E-17, 0.000000000000000000, -1.000000000000000000 ) ) ;
#9642=FACE_OUTER_BOUND ( 'NONE', #37583, .T. ) ;
#9712=EDGE_LOOP ( 'NONE', ( #175488, #136539, #193559, #70664 ) ) ;
#9723=DIRECTION ( 'NONE',  ( 0.000000000000000000, 1.000000000000000000, 0.000000000000000000 ) ) ;
#9851=DIRECTION ( 'NONE',  ( 0.000000000000000000, -1.000000000000000000, 0.000000000000000000 ) ) ;
#9913=EDGE_CURVE ( 'NONE', #150798, #157913, #117534, .T. ) ;
#9977=DIRECTION ( 'NONE',  ( -5.551115123125764829E-17, 0.000000000000000000, 1.000000000000000000 ) ) ;
#10104=CARTESIAN_POINT ( 'NONE',  ( 1.841222038795641122E-16, 2.000000000000001776, 2.750000000000008438 ) ) ;
#10105=EDGE_LOOP ( 'NONE', ( #185826, #183591, #177194, #70564 ) ) ;
#10457=VERTEX_POINT ( 'NONE', #177684 ) ;
#10534=ORIENTED_EDGE ( 'NONE', *, *, #86344, .F. ) ;
#10566=EDGE_CURVE ( 'NONE', #105092, #73686, #214205, .T. ) ;
#11057=DIRECTION ( 'NONE',  ( 0.000000000000000000, 1.000000000000000000, 0.000000000000000000 ) ) ;
#11430=CARTESIAN_POINT ( 'NONE',  ( 0.000000000000000000, 2.099999999999997868, 0.000000000000000000 ) ) ;
#11986=ORIENTED_EDGE ( 'NONE', *, *, #17877, .F. ) ;
#12024=EDGE_CURVE ( 'NONE', #121388, #57555, #62280, .T. ) ;
#12053=ORIENTED_EDGE ( 'NONE', *, *, #141945, .F. ) ;
#12143=CARTESIAN_POINT ( 'NONE',  ( -0.6170404364503389028, 3.500000000000003109, 1.902435570468863801 ) ) ;
#12384=FACE_OUTER_BOUND ( 'NONE', #87810, .T. ) ;
#12395=ADVANCED_FACE ( 'NONE', ( #4619, #70691 ), #88045, .T. ) ;
#13017=DIRECTION ( 'NONE',  ( -5.551115123125764829E-17, 0.000000000000000000, 1.000000000000000000 ) ) ;
#13191=MANIFOLD_SOLID_BREP ( 'Cut-Revolve1', #101781 ) ;
#13787=DIRECTION ( 'NONE',  ( 0.000000000000000000, 1.000000000000000000, 0.000000000000000000 ) ) ;
#13801=( GEOMETRIC_REPRESENTATION_CONTEXT ( 3 ) GLOBAL_UNCERTAINTY_ASSIGNED_CONTEXT ( ( #7300 ) ) GLOBAL_UNIT_ASSIGNED_CONTEXT ( ( #207618, #191359, #92839 ) ) REPRESENTATION_CONTEXT ( 'NONE', 'WORKASPACE' ) );
#14105=CIRCLE ( 'NONE', #3724, 2.500000000000007994 ) ;
#14836=CYLINDRICAL_SURFACE ( 'NONE', #179373, 2.000000000000006661 ) ;
#14905=ORIENTED_EDGE ( 'NONE', *, *, #181245, .F. ) ;
#14997=DIRECTION ( 'NONE',  ( 0.000000000000000000, -1.000000000000000000, 0.000000000000000000 ) ) ;
#15026=EDGE_LOOP ( 'NONE', ( #96487, #105535, #52255, #94848 ) ) ;
#15092=ADVANCED_FACE ( 'NONE', ( #118050 ), #117385, .T. ) ;
#15704=DIRECTION ( 'NONE',  ( 5.551115123125764213E-17, 0.000000000000000000, -1.000000000000000000 ) ) ;
#15946=CIRCLE ( 'NONE', #137057, 2.250000000000006661 ) ;
#15967=CARTESIAN_POINT ( 'NONE',  ( 4.182432031930846947E-16, 4.099999999999999645, -2.350000000000007194 ) ) ;
#16232=CARTESIAN_POINT ( 'NONE',  ( 0.000000000000000000, -0.5000000000000004441, 0.000000000000000000 ) ) ;
#16348=ADVANCED_FACE ( 'NONE', ( #5806, #122899 ), #56731, .T. ) ;
#16374=CARTESIAN_POINT ( 'NONE',  ( 0.000000000000000000, 4.400000000000001243, 0.000000000000000000 ) ) ;
#16428=EDGE_CURVE ( 'NONE', #34978, #36555, #15946, .T. ) ;
#16464=FACE_OUTER_BOUND ( 'NONE', #214224, .T. ) ;
#16499=CIRCLE ( 'NONE', #179041, 0.09999999999999982514 ) ;
#16562=ADVANCED_FACE ( 'NONE', ( #105506 ), #190974, .T. ) ;
#16969=CARTESIAN_POINT ( 'NONE',  ( 0.000000000000000000, 1.899999999999999023, 0.000000000000000000 ) ) ;
#16987=ORIENTED_EDGE ( 'NONE', *, *, #109243, .T. ) ;
#17102=EDGE_LOOP ( 'NONE', ( #199387, #158418, #71365, #154063 ) ) ;
#17253=AXIS2_PLACEMENT_3D ( 'NONE', #197110, #100676, #147318 ) ;
#17309=DIRECTION ( 'NONE',  ( -5.551115123125765446E-17, 0.000000000000000000, 1.000000000000000000 ) ) ;
#17524=CYLINDRICAL_SURFACE ( 'NONE', #4335, 2.250000000000006661 ) ;
#17877=EDGE_CURVE ( 'NONE', #194213, #170139, #3054, .T. ) ;
#17912=FACE_OUTER_BOUND ( 'NONE', #99877, .T. ) ;
#18249=CARTESIAN_POINT ( 'NONE',  ( 1.355808955840426748E-16, 3.500000000000003109, 2.025000000000006573 ) ) ;
#18254=ORIENTED_EDGE ( 'NONE', *, *, #21174, .F. ) ;
#18291=EDGE_CURVE ( 'NONE', #106, #136049, #85403, .T. ) ;
#18358=DIRECTION ( 'NONE',  ( -9.577770318032057676E-19, 0.9998511425080263137, 0.01725377713413180428 ) ) ;
#18394=CARTESIAN_POINT ( 'NONE',  ( 0.000000000000000000, 3.400000000000000355, 0.000000000000000000 ) ) ;
#18403=ORIENTED_EDGE ( 'NONE', *, *, #91003, .F. ) ;
#18607=EDGE_CURVE ( 'NONE', #59046, #140877, #213402, .T. ) ;
#18842=AXIS2_PLACEMENT_3D ( 'NONE', #69117, #65911, #51842 ) ;
#19050=ORIENTED_EDGE ( 'NONE', *, *, #117783, .T. ) ;
#19213=DIRECTION ( 'NONE',  ( -1.000000000000000000, 0.000000000000000000, -5.551115123125765446E-17 ) ) ;
#19322=CARTESIAN_POINT ( 'NONE',  ( 0.000000000000000000, 1.500000000000001332, 0.000000000000000000 ) ) ;
#19335=FACE_OUTER_BOUND ( 'NONE', #210722, .T. ) ;
#19682=AXIS2_PLACEMENT_3D ( 'NONE', #32608, #49927, #101873 ) ;
#19719=DIRECTION ( 'NONE',  ( 0.000000000000000000, 1.000000000000000000, 0.000000000000000000 ) ) ;
#19843=ORIENTED_EDGE ( 'NONE', *, *, #54959, .T. ) ;
#19862=CIRCLE ( 'NONE', #37190, 2.250000000000006661 ) ;
#19939=CYLINDRICAL_SURFACE ( 'NONE', #105935, 2.500000000000007994 ) ;
#19949=EDGE_CURVE ( 'NONE', #132709, #147669, #154681, .T. ) ;
#20031=( NAMED_UNIT ( * ) SI_UNIT ( $, .STERADIAN. ) SOLID_ANGLE_UNIT ( ) );
#20387=DIRECTION ( 'NONE',  ( 2.433448702482861237E-17, -0.8987940462991643731, -0.4383711467890826219 ) ) ;
#20495=DIRECTION ( 'NONE',  ( 0.000000000000000000, 1.000000000000000000, 0.000000000000000000 ) ) ;
#20893=DIRECTION ( 'NONE',  ( -0.000000000000000000, -1.000000000000000000, -0.000000000000000000 ) ) ;
#21174=EDGE_CURVE ( 'NONE', #87955, #132709, #103772, .T. ) ;
#21234=FACE_OUTER_BOUND ( 'NONE', #84959, .T. ) ;
#21304=CIRCLE ( 'NONE', #211509, 2.400000000000007461 ) ;
#21644=ORIENTED_EDGE ( 'NONE', *, *, #178677, .T. ) ;
#22146=DIRECTION ( 'NONE',  ( 0.000000000000000000, -1.000000000000000000, 0.000000000000000000 ) ) ;
#22368=AXIS2_PLACEMENT_3D ( 'NONE', #58863, #26351, #159565 ) ;
#22451=PRESENTATION_STYLE_ASSIGNMENT (( #58180 ) ) ;
#22734=DIRECTION ( 'NONE',  ( -5.551115123125764829E-17, 0.000000000000000000, 1.000000000000000000 ) ) ;
#23130=DIRECTION ( 'NONE',  ( 5.551115123125766062E-17, 0.000000000000000000, -1.000000000000000000 ) ) ;
#23409=CARTESIAN_POINT ( 'NONE',  ( 0.000000000000000000, 3.900000000000000799, 0.000000000000000000 ) ) ;
#23436=DIRECTION ( 'NONE',  ( -0.3085202182251676195, 0.000000000000000000, 0.9512177852344304574 ) ) ;
#23641=CARTESIAN_POINT ( 'NONE',  ( 0.000000000000000000, 4.400000000000001243, 0.000000000000000000 ) ) ;
#23708=CARTESIAN_POINT ( 'NONE',  ( 8.326672684688649401E-17, 4.400000000000001243, -1.500000000000000222 ) ) ;
#23971=DIRECTION ( 'NONE',  ( 0.000000000000000000, -1.000000000000000000, 0.000000000000000000 ) ) ;
#24200=AXIS2_PLACEMENT_3D ( 'NONE', #16969, #131859, #46319 ) ;
#24587=DIRECTION ( 'NONE',  ( 0.000000000000000000, -1.000000000000000000, 0.000000000000000000 ) ) ;
#24815=DIRECTION ( 'NONE',  ( 0.000000000000000000, -1.000000000000000000, 0.000000000000000000 ) ) ;
#24949=ADVANCED_FACE ( 'NONE', ( #187209 ), #71304, .F. ) ;
#25161=CARTESIAN_POINT ( 'NONE',  ( 0.000000000000000000, 4.099999999999999645, 0.000000000000000000 ) ) ;
#25558=CARTESIAN_POINT ( 'NONE',  ( 0.6170404364503341288, -1.000000000000000888, -1.902435570468864690 ) ) ;
#25737=EDGE_CURVE ( 'NONE', #142577, #195087, #89960, .T. ) ;
#25775=DIRECTION ( 'NONE',  ( -0.000000000000000000, -1.000000000000000000, -0.000000000000000000 ) ) ;
#25938=AXIS2_PLACEMENT_3D ( 'NONE', #11430, #127421, #193392 ) ;
#26124=CARTESIAN_POINT ( 'NONE',  ( 4.360407863076827793E-16, 4.000000000000003553, -2.400000000000000355 ) ) ;
#26308=ADVANCED_FACE ( 'NONE', ( #95397 ), #184068, .T. ) ;
#26351=DIRECTION ( 'NONE',  ( 0.000000000000000000, -1.000000000000000000, 0.000000000000000000 ) ) ;
#26392=ORIENTED_EDGE ( 'NONE', *, *, #1866, .T. ) ;
#26509=DIRECTION ( 'NONE',  ( 0.000000000000000000, 1.000000000000000000, 0.000000000000000000 ) ) ;
#26695=EDGE_CURVE ( 'NONE', #202678, #78316, #86573, .T. ) ;
#26953=AXIS2_PLACEMENT_3D ( 'NONE', #110678, #161510, #95461 ) ;
#27014=DIRECTION ( 'NONE',  ( 0.000000000000000000, 1.000000000000000000, 0.000000000000000000 ) ) ;
#27074=EDGE_CURVE ( 'NONE', #147669, #132709, #153003, .T. ) ;
#27472=ADVANCED_FACE ( 'NONE', ( #161171 ), #64718, .T. ) ;
#27774=EDGE_LOOP ( 'NONE', ( #26392, #129913 ) ) ;
#27829=CIRCLE ( 'NONE', #139027, 2.025000000000006573 ) ;
#27910=DIRECTION ( 'NONE',  ( -0.000000000000000000, -1.000000000000000000, -0.000000000000000000 ) ) ;
#28283=DIRECTION ( 'NONE',  ( 0.000000000000000000, -1.000000000000000000, 0.000000000000000000 ) ) ;
#28767=ORIENTED_EDGE ( 'NONE', *, *, #55350, .F. ) ;
#29021=CARTESIAN_POINT ( 'NONE',  ( 1.355808955840422310E-16, -0.5000000000000004441, 2.024999999999999911 ) ) ;
#29351=CIRCLE ( 'NONE', #157227, 2.350000000000007194 ) ;
#29472=VERTEX_POINT ( 'NONE', #5311 ) ;
#29814=APPLICATION_CONTEXT ( 'automotive_design' ) ;
#30059=CARTESIAN_POINT ( 'NONE',  ( 0.000000000000000000, 1.899999999999999023, 0.000000000000000000 ) ) ;
#30215=CARTESIAN_POINT ( 'NONE',  ( 0.000000000000000000, 3.500000000000003109, 0.000000000000000000 ) ) ;
#30646=DIRECTION ( 'NONE',  ( 3.070755325854836401E-18, 0.9998511425080263137, -0.01725377713413180428 ) ) ;
#30748=EDGE_LOOP ( 'NONE', ( #21644, #7939, #46642, #53862, #58105 ) ) ;
#30996=CARTESIAN_POINT ( 'NONE',  ( 0.000000000000000000, 3.400000000000000355, 0.000000000000000000 ) ) ;
#31001=MECHANICAL_DESIGN_GEOMETRIC_PRESENTATION_REPRESENTATION('',(#121051),#93323);
#31316=EDGE_CURVE ( 'NONE', #180001, #191870, #101347, .T. ) ;
#31468=EDGE_CURVE ( 'NONE', #73686, #10457, #156727, .T. ) ;
#31526=CARTESIAN_POINT ( 'NONE',  ( 0.000000000000000000, 4.099999999999999645, 0.000000000000000000 ) ) ;
#31594=ORIENTED_EDGE ( 'NONE', *, *, #64213, .T. ) ;
#31600=ORIENTED_EDGE ( 'NONE', *, *, #169914, .T. ) ;
#32009=CARTESIAN_POINT ( 'NONE',  ( 0.000000000000000000, 4.000000000000003553, 0.000000000000000000 ) ) ;
#32065=ORIENTED_EDGE ( 'NONE', *, *, #122192, .F. ) ;
#32419=AXIS2_PLACEMENT_3D ( 'NONE', #31526, #143182, #128047 ) ;
#32608=CARTESIAN_POINT ( 'NONE',  ( 0.000000000000000000, 3.500000000000003109, 0.000000000000000000 ) ) ;
#32776=ORIENTED_EDGE ( 'NONE', *, *, #115310, .T. ) ;
#32942=EDGE_LOOP ( 'NONE', ( #102992, #210329 ) ) ;
#32992=ADVANCED_FACE ( 'NONE', ( #207184 ), #193064, .F. ) ;
#33234=CARTESIAN_POINT ( 'NONE',  ( -3.469446951953614189E-15, -1.000000000000000888, 2.602085213965210642E-15 ) ) ;
#33453=AXIS2_PLACEMENT_3D ( 'NONE', #171538, #72961, #23130 ) ;
#33529=DIRECTION ( 'NONE',  ( -5.551115123125765446E-17, 0.000000000000000000, 1.000000000000000000 ) ) ;
#34205=UNCERTAINTY_MEASURE_WITH_UNIT (LENGTH_MEASURE( 1.000000000000000082E-05 ), #105597, 'distance_accuracy_value', 'NONE');
#34501=EDGE_CURVE ( 'NONE', #34978, #165933, #47990, .T. ) ;
#34512=DIRECTION ( 'NONE',  ( -0.000000000000000000, 1.000000000000000000, -0.000000000000000000 ) ) ;
#34653=DIRECTION ( 'NONE',  ( 0.000000000000000000, -1.000000000000000000, 0.000000000000000000 ) ) ;
#34699=EDGE_LOOP ( 'NONE', ( #142438, #95917 ) ) ;
#34880=ORIENTED_EDGE ( 'NONE', *, *, #10566, .T. ) ;
#34930=ADVANCED_FACE ( 'NONE', ( #175554 ), #75904, .T. ) ;
#34978=VERTEX_POINT ( 'NONE', #192833 ) ;
#35220=CARTESIAN_POINT ( 'NONE',  ( 0.000000000000000000, 3.900000000000000799, 0.000000000000000000 ) ) ;
#35573=DIRECTION ( 'NONE',  ( 5.551115123125764213E-17, 0.000000000000000000, -1.000000000000000000 ) ) ;
#35587=FACE_BOUND ( 'NONE', #194547, .T. ) ;
#36130=CIRCLE ( 'NONE', #181464, 0.09999999999999982514 ) ;
#36169=ADVANCED_FACE ( 'NONE', ( #132175 ), #165766, .F. ) ;
#36307=CARTESIAN_POINT ( 'NONE',  ( 0.000000000000000000, 1.750000000000001554, 0.000000000000000000 ) ) ;
#36555=VERTEX_POINT ( 'NONE', #105280 ) ;
#36609=CARTESIAN_POINT ( 'NONE',  ( 0.000000000000000000, 4.400000000000001243, 0.000000000000000000 ) ) ;
#37051=ORIENTED_EDGE ( 'NONE', *, *, #57845, .F. ) ;
#37090=LINE ( 'NONE', #188681, #78022 ) ;
#37190=AXIS2_PLACEMENT_3D ( 'NONE', #52763, #153477, #5049 ) ;
#37273=DIRECTION ( 'NONE',  ( 5.551115123125764829E-17, 0.000000000000000000, -1.000000000000000000 ) ) ;
#37583=EDGE_LOOP ( 'NONE', ( #113904, #170117, #51081, #184931 ) ) ;
#37629=CARTESIAN_POINT ( 'NONE',  ( 0.000000000000000000, 3.599999999999999201, 0.000000000000000000 ) ) ;
#37889=DIRECTION ( 'NONE',  ( 0.000000000000000000, -1.000000000000000000, 0.000000000000000000 ) ) ;
#38009=AXIS2_PLACEMENT_3D ( 'NONE', #75246, #57922, #207372 ) ;
#38433=DIRECTION ( 'NONE',  ( 5.551115123125764829E-17, 0.000000000000000000, -1.000000000000000000 ) ) ;
#38632=ORIENTED_EDGE ( 'NONE', *, *, #127735, .T. ) ;
#38915=AXIS2_PLACEMENT_3D ( 'NONE', #135616, #6645, #184337 ) ;
#38959=CYLINDRICAL_SURFACE ( 'NONE', #39586, 2.750000000000008438 ) ;
#39008=CARTESIAN_POINT ( 'NONE',  ( 0.000000000000000000, 1.500000000000001332, 0.000000000000000000 ) ) ;
#39133=ORIENTED_EDGE ( 'NONE', *, *, #93452, .F. ) ;
#39268=EDGE_CURVE ( 'NONE', #140877, #59046, #165429, .T. ) ;
#39481=ADVANCED_FACE ( 'NONE', ( #108165 ), #14836, .F. ) ;
#39586=AXIS2_PLACEMENT_3D ( 'NONE', #107219, #37889, #7497 ) ;
#39637=EDGE_CURVE ( 'NONE', #206340, #197886, #175824, .T. ) ;
#39802=FILL_AREA_STYLE_COLOUR ( '', #165964 ) ;
#40583=CARTESIAN_POINT ( 'NONE',  ( 0.000000000000000000, 0.000000000000000000, 0.000000000000000000 ) ) ;
#40640=DIRECTION ( 'NONE',  ( 0.3085202182251676195, 0.000000000000000000, -0.9512177852344304574 ) ) ;
#41213=EDGE_LOOP ( 'NONE', ( #161177, #163758, #28767, #79411, #78012 ) ) ;
#41937=VECTOR ( 'NONE', #23971, 1000.000000000000000 ) ;
#42083=DIRECTION ( 'NONE',  ( 1.000000000000000000, -0.000000000000000000, 1.779758311459929752E-16 ) ) ;
#42161=CARTESIAN_POINT ( 'NONE',  ( 8.881784197001254049E-17, 3.500000000000000888, -1.600000000000005196 ) ) ;
#42253=CARTESIAN_POINT ( 'NONE',  ( -1.471045507628332367E-16, 2.000000000000001776, 2.650000000000008349 ) ) ;
#42382=ORIENTED_EDGE ( 'NONE', *, *, #115310, .F. ) ;
#42520=EDGE_CURVE ( 'NONE', #195087, #142577, #75757, .T. ) ;
#42683=ORIENTED_EDGE ( 'NONE', *, *, #188635, .F. ) ;
#43165=CIRCLE ( 'NONE', #18842, 0.09999999999999982514 ) ;
#43237=CARTESIAN_POINT ( 'NONE',  ( 0.000000000000000000, 2.999999999999975131, 0.000000000000000000 ) ) ;
#43257=AXIS2_PLACEMENT_3D ( 'NONE', #18394, #34653, #166802 ) ;
#43463=EDGE_CURVE ( 'NONE', #170139, #145077, #675, .T. ) ;
#43741=ORIENTED_EDGE ( 'NONE', *, *, #43463, .T. ) ;
#44058=ORIENTED_EDGE ( 'NONE', *, *, #27074, .F. ) ;
#44166=DIRECTION ( 'NONE',  ( -5.551115123125765446E-17, 0.000000000000000000, 1.000000000000000000 ) ) ;
#44254=TOROIDAL_SURFACE ( 'NONE', #151554, 2.400000000000000355, 0.1000000000000000056 ) ;
#44293=CARTESIAN_POINT ( 'NONE',  ( -1.443289932012703552E-16, 2.099999999999997868, 2.600000000000008082 ) ) ;
#44770=CARTESIAN_POINT ( 'NONE',  ( 3.559516622919870350E-16, 1.551257596039481879, -2.000000000000006217 ) ) ;
#45681=AXIS2_PLACEMENT_3D ( 'NONE', #172221, #6484, #173294 ) ;
#45838=AXIS2_PLACEMENT_3D ( 'NONE', #16374, #66175, #112907 ) ;
#46147=DIRECTION ( 'NONE',  ( -0.000000000000000000, 1.000000000000000000, -0.000000000000000000 ) ) ;
#46319=DIRECTION ( 'NONE',  ( -5.551115123125765446E-17, 0.000000000000000000, 1.000000000000000000 ) ) ;
#46322=FACE_OUTER_BOUND ( 'NONE', #60645, .T. ) ;
#46402=ADVANCED_FACE ( 'NONE', ( #192313 ), #44254, .T. ) ;
#46605=CARTESIAN_POINT ( 'NONE',  ( 4.182432031930847440E-16, 4.000000000000001776, -2.350000000000007194 ) ) ;
#46642=ORIENTED_EDGE ( 'NONE', *, *, #156015, .T. ) ;
#46803=DIRECTION ( 'NONE',  ( -5.551115123125764829E-17, 0.000000000000000000, 1.000000000000000000 ) ) ;
#46857=CIRCLE ( 'NONE', #129933, 2.150000000000006573 ) ;
#46885=DIRECTION ( 'NONE',  ( 5.551115123125766062E-17, 0.000000000000000000, -1.000000000000000000 ) ) ;
#46989=DIRECTION ( 'NONE',  ( -1.000000000000000000, 0.000000000000000000, -5.551115123125765446E-17 ) ) ;
#47196=ORIENTED_EDGE ( 'NONE', *, *, #165187, .T. ) ;
#47436=DIRECTION ( 'NONE',  ( 5.551115123125765446E-17, 0.000000000000000000, -1.000000000000000000 ) ) ;
#47478=CARTESIAN_POINT ( 'NONE',  ( 8.326672684688675286E-17, 6.999999999999999112, -1.500000000000005107 ) ) ;
#47506=DIRECTION ( 'NONE',  ( -5.551115123125782702E-17, 0.000000000000000000, 1.000000000000000000 ) ) ;
#47776=CIRCLE ( 'NONE', #58098, 0.09999999999999982514 ) ;
#47990=CIRCLE ( 'NONE', #148307, 0.09999999999999982514 ) ;
#48801=ORIENTED_EDGE ( 'NONE', *, *, #211272, .T. ) ;
#48835=EDGE_LOOP ( 'NONE', ( #177561, #123838 ) ) ;
#48921=ORIENTED_EDGE ( 'NONE', *, *, #53808, .F. ) ;
#49059=ORIENTED_EDGE ( 'NONE', *, *, #159020, .T. ) ;
#49473=LINE ( 'NONE', #129747, #157108 ) ;
#49793=ORIENTED_EDGE ( 'NONE', *, *, #119633, .T. ) ;
#49927=DIRECTION ( 'NONE',  ( -0.000000000000000000, 1.000000000000000000, -0.000000000000000000 ) ) ;
#50214=DIRECTION ( 'NONE',  ( 5.551115123125765446E-17, 0.000000000000000000, -1.000000000000000000 ) ) ;
#50260=EDGE_LOOP ( 'NONE', ( #32065, #157965, #180514, #207777, #72193 ) ) ;
#50360=EDGE_LOOP ( 'NONE', ( #86838, #16987, #59676, #48921 ) ) ;
#50758=CARTESIAN_POINT ( 'NONE',  ( 8.326672684688675286E-17, 3.599999999999999201, -1.500000000000005107 ) ) ;
#50914=FACE_OUTER_BOUND ( 'NONE', #41213, .T. ) ;
#50964=ORIENTED_EDGE ( 'NONE', *, *, #167075, .T. ) ;
#51000=AXIS2_PLACEMENT_3D ( 'NONE', #54317, #104138, #134531 ) ;
#51081=ORIENTED_EDGE ( 'NONE', *, *, #9913, .T. ) ;
#51084=CARTESIAN_POINT ( 'NONE',  ( 1.347439764754987941E-16, 3.466143782776612170, 2.000000000000000000 ) ) ;
#51402=DIRECTION ( 'NONE',  ( 0.000000000000000000, -1.000000000000000000, 0.000000000000000000 ) ) ;
#51701=CYLINDRICAL_SURFACE ( 'NONE', #209269, 2.000000000000006661 ) ;
#51751=AXIS2_PLACEMENT_3D ( 'NONE', #103842, #137417, #55090 ) ;
#51842=DIRECTION ( 'NONE',  ( 1.779758311459934189E-16, 0.000000000000000000, -1.000000000000000000 ) ) ;
#51848=CARTESIAN_POINT ( 'NONE',  ( 1.056414318722240136E-16, 1.750000000000001554, -1.903066852858540603 ) ) ;
#52128=CIRCLE ( 'NONE', #104081, 0.1000000000000000472 ) ;
#52190=DIRECTION ( 'NONE',  ( 0.000000000000000000, 1.000000000000000000, 0.000000000000000000 ) ) ;
#52255=ORIENTED_EDGE ( 'NONE', *, *, #190193, .F. ) ;
#52425=AXIS2_PLACEMENT_3D ( 'NONE', #60446, #122355, #190439 ) ;
#52720=LINE ( 'NONE', #102541, #129793 ) ;
#52763=CARTESIAN_POINT ( 'NONE',  ( 0.000000000000000000, 4.099999999999999645, 0.000000000000000000 ) ) ;
#53584=TOROIDAL_SURFACE ( 'NONE', #1764, 1.600000000000000311, 0.1000000000000000056 ) ;
#53604=CARTESIAN_POINT ( 'NONE',  ( 1.526556658859585313E-16, 1.899999999999999023, -2.750000000000000000 ) ) ;
#53647=ADVANCED_FACE ( 'NONE', ( #16464 ), #17524, .T. ) ;
#53660=SHAPE_DEFINITION_REPRESENTATION ( #159541, #142805 ) ;
#53808=EDGE_CURVE ( 'NONE', #184764, #9073, #4463, .T. ) ;
#53862=ORIENTED_EDGE ( 'NONE', *, *, #169914, .F. ) ;
#54264=DIRECTION ( 'NONE',  ( -6.695352868347761696E-17, 0.000000000000000000, -1.000000000000000000 ) ) ;
#54308=EDGE_LOOP ( 'NONE', ( #174420, #211180, #138405, #189321 ) ) ;
#54317=CARTESIAN_POINT ( 'NONE',  ( 0.000000000000000000, 4.400000000000001243, 0.000000000000000000 ) ) ;
#54364=LINE ( 'NONE', #55421, #107693 ) ;
#54959=EDGE_CURVE ( 'NONE', #184764, #111689, #160222, .T. ) ;
#55090=DIRECTION ( 'NONE',  ( 5.551115123125764213E-17, 0.000000000000000000, -1.000000000000000000 ) ) ;
#55350=EDGE_CURVE ( 'NONE', #191870, #77536, #104892, .T. ) ;
#55421=CARTESIAN_POINT ( 'NONE',  ( 1.526556658859590243E-16, 2.000000000000001776, -2.750000000000008438 ) ) ;
#55657=DIRECTION ( 'NONE',  ( 0.000000000000000000, 1.000000000000000000, 0.000000000000000000 ) ) ;
#55705=CIRCLE ( 'NONE', #118089, 3.000000000000010214 ) ;
#56069=AXIS2_PLACEMENT_3D ( 'NONE', #8511, #77777, #173176 ) ;
#56091=CIRCLE ( 'NONE', #173771, 0.1000000000000000472 ) ;
#56731=PLANE ( 'NONE',  #109450 ) ;
#57159=CIRCLE ( 'NONE', #91819, 2.350000000000007194 ) ;
#57203=CARTESIAN_POINT ( 'NONE',  ( 0.000000000000000000, -0.5000000000000004441, 0.000000000000000000 ) ) ;
#57246=DIRECTION ( 'NONE',  ( 1.779758311459929505E-16, 0.000000000000000000, -1.000000000000000000 ) ) ;
#57298=CIRCLE ( 'NONE', #84966, 0.1000000000000000472 ) ;
#57465=EDGE_CURVE ( 'NONE', #36555, #34978, #200864, .T. ) ;
#57544=EDGE_LOOP ( 'NONE', ( #18403, #1270, #47196, #166621 ) ) ;
#57555=VERTEX_POINT ( 'NONE', #123387 ) ;
#57658=ADVANCED_FACE ( 'NONE', ( #46322 ), #173247, .T. ) ;
#57845=EDGE_CURVE ( 'NONE', #197886, #206340, #14105, .T. ) ;
#57922=DIRECTION ( 'NONE',  ( -0.000000000000000000, -1.000000000000000000, -0.000000000000000000 ) ) ;
#57979=ORIENTED_EDGE ( 'NONE', *, *, #39637, .F. ) ;
#58098=AXIS2_PLACEMENT_3D ( 'NONE', #15967, #151346, #147084 ) ;
#58105=ORIENTED_EDGE ( 'NONE', *, *, #157474, .F. ) ;
#58180=SURFACE_STYLE_USAGE ( .BOTH. , #90704 ) ;
#58272=DIRECTION ( 'NONE',  ( 0.000000000000000000, -1.000000000000000000, 0.000000000000000000 ) ) ;
#58325=PLANE ( 'NONE',  #52425 ) ;
#58443=AXIS2_PLACEMENT_3D ( 'NONE', #109735, #212475, #61987 ) ;
#58613=ORIENTED_EDGE ( 'NONE', *, *, #105847, .F. ) ;
#58650=CARTESIAN_POINT ( 'NONE',  ( -1.443289932012703552E-16, 1.999999999999999556, 2.600000000000008082 ) ) ;
#58863=CARTESIAN_POINT ( 'NONE',  ( 0.000000000000000000, 3.500000000000003109, 0.000000000000000000 ) ) ;
#59046=VERTEX_POINT ( 'NONE', #90882 ) ;
#59330=FACE_OUTER_BOUND ( 'NONE', #164123, .T. ) ;
#59537=CARTESIAN_POINT ( 'NONE',  ( 0.000000000000000000, 0.000000000000000000, 0.000000000000000000 ) ) ;
#59676=ORIENTED_EDGE ( 'NONE', *, *, #70880, .T. ) ;
#60017=DIRECTION ( 'NONE',  ( 0.000000000000000000, -1.000000000000000000, 0.000000000000000000 ) ) ;
#60036=CIRCLE ( 'NONE', #146516, 1.600000000000005196 ) ;
#60288=EDGE_CURVE ( 'NONE', #181670, #91753, #101653, .T. ) ;
#60393=AXIS2_PLACEMENT_3D ( 'NONE', #136726, #187585, #203816 ) ;
#60446=CARTESIAN_POINT ( 'NONE',  ( 0.000000000000000000, 4.500000000000003553, 0.000000000000000000 ) ) ;
#60529=EDGE_CURVE ( 'NONE', #181670, #170139, #166566, .T. ) ;
#60530=DIRECTION ( 'NONE',  ( 5.551115123125764829E-17, 0.000000000000000000, -1.000000000000000000 ) ) ;
#60581=FACE_OUTER_BOUND ( 'NONE', #197364, .T. ) ;
#60645=EDGE_LOOP ( 'NONE', ( #8863, #188447, #129299, #112662 ) ) ;
#60943=DIRECTION ( 'NONE',  ( 5.551115123125764829E-17, 0.000000000000000000, -1.000000000000000000 ) ) ;
#60996=LINE ( 'NONE', #44770, #206068 ) ;
#61085=CARTESIAN_POINT ( 'NONE',  ( -8.881784197001254049E-17, 4.400000000000001243, 1.600000000000005196 ) ) ;
#61348=FACE_OUTER_BOUND ( 'NONE', #50260, .T. ) ;
#61624=ADVANCED_FACE ( 'NONE', ( #190574 ), #108346, .F. ) ;
#61987=DIRECTION ( 'NONE',  ( -5.551115123125765446E-17, 0.000000000000000000, 1.000000000000000000 ) ) ;
#62074=LINE ( 'NONE', #10104, #126241 ) ;
#62145=EDGE_CURVE ( 'NONE', #146253, #107037, #208293, .T. ) ;
#62280=CIRCLE ( 'NONE', #38009, 1.600000000000005196 ) ;
#62788=EDGE_CURVE ( 'NONE', #166237, #87955, #104577, .T. ) ;
#63498=AXIS2_PLACEMENT_3D ( 'NONE', #40583, #60017, #38433 ) ;
#63599=DIRECTION ( 'NONE',  ( 0.000000000000000000, 1.000000000000000000, 0.000000000000000000 ) ) ;
#63700=LINE ( 'NONE', #47478, #101999 ) ;
#63808=CARTESIAN_POINT ( 'NONE',  ( 0.000000000000000000, -0.5000000000000004441, 0.000000000000000000 ) ) ;
#63823=ORIENTED_EDGE ( 'NONE', *, *, #57465, .T. ) ;
#63997=CIRCLE ( 'NONE', #25938, 2.500000000000007994 ) ;
#64175=AXIS2_PLACEMENT_3D ( 'NONE', #212318, #2112, #17309 ) ;
#64213=EDGE_CURVE ( 'NONE', #197886, #168244, #184168, .T. ) ;
#64246=ORIENTED_EDGE ( 'NONE', *, *, #16428, .T. ) ;
#64342=ORIENTED_EDGE ( 'NONE', *, *, #92035, .T. ) ;
#64475=CIRCLE ( 'NONE', #143990, 2.025000000000006573 ) ;
#64480=FACE_OUTER_BOUND ( 'NONE', #202315, .T. ) ;
#64559=CIRCLE ( 'NONE', #133856, 1.500000000000005107 ) ;
#64718=CYLINDRICAL_SURFACE ( 'NONE', #170163, 2.750000000000008438 ) ;
#65245=EDGE_CURVE ( 'NONE', #174590, #149924, #83977, .T. ) ;
#65360=CARTESIAN_POINT ( 'NONE',  ( 1.355808955840427734E-16, 1.500000000000001332, 2.025000000000007905 ) ) ;
#65911=DIRECTION ( 'NONE',  ( 1.000000000000000000, -0.000000000000000000, 1.779758311459929752E-16 ) ) ;
#65939=CARTESIAN_POINT ( 'NONE',  ( 1.355808955840422310E-16, 3.400000000000000355, 2.024999999999999911 ) ) ;
#66175=DIRECTION ( 'NONE',  ( 0.000000000000000000, 1.000000000000000000, 0.000000000000000000 ) ) ;
#66440=CARTESIAN_POINT ( 'NONE',  ( 0.000000000000000000, 4.500000000000003553, 0.000000000000000000 ) ) ;
#66579=ORIENTED_EDGE ( 'NONE', *, *, #18291, .F. ) ;
#67830=DIRECTION ( 'NONE',  ( -0.3085202182251676195, 0.000000000000000000, 0.9512177852344304574 ) ) ;
#68241=ORIENTED_EDGE ( 'NONE', *, *, #162949, .F. ) ;
#68250=DIRECTION ( 'NONE',  ( 0.000000000000000000, 1.000000000000000000, 0.000000000000000000 ) ) ;
#68277=CARTESIAN_POINT ( 'NONE',  ( -1.332267629550188046E-16, 3.900000000000000799, 2.400000000000007461 ) ) ;
#68739=CARTESIAN_POINT ( 'NONE',  ( 4.805347440941809738E-16, 2.000000000000001776, -2.649999999999999911 ) ) ;
#69117=CARTESIAN_POINT ( 'NONE',  ( 4.716359525368828436E-16, 1.899999999999999023, -2.650000000000008349 ) ) ;
#69252=DIRECTION ( 'NONE',  ( -6.695352868347761696E-17, 0.000000000000000000, -1.000000000000000000 ) ) ;
#69687=DIRECTION ( 'NONE',  ( -5.551115123125782702E-17, 0.000000000000000000, 1.000000000000000000 ) ) ;
#69877=PRODUCT_CONTEXT ( 'NONE', #156970, 'mechanical' ) ;
#70013=FACE_OUTER_BOUND ( 'NONE', #207670, .T. ) ;
#70564=ORIENTED_EDGE ( 'NONE', *, *, #211272, .F. ) ;
#70635=DIRECTION ( 'NONE',  ( 0.000000000000000000, -1.000000000000000000, 0.000000000000000000 ) ) ;
#70664=ORIENTED_EDGE ( 'NONE', *, *, #19949, .F. ) ;
#70691=FACE_OUTER_BOUND ( 'NONE', #77394, .T. ) ;
#70880=EDGE_CURVE ( 'NONE', #205992, #9073, #55705, .T. ) ;
#71265=EDGE_LOOP ( 'NONE', ( #168377, #162085, #147301, #182738 ) ) ;
#71304=CYLINDRICAL_SURFACE ( 'NONE', #51751, 2.025000000000006573 ) ;
#71365=ORIENTED_EDGE ( 'NONE', *, *, #162949, .T. ) ;
#71547=ADVANCED_FACE ( 'NONE', ( #35587, #19335 ), #87558, .T. ) ;
#71763=DIRECTION ( 'NONE',  ( 0.000000000000000000, -1.000000000000000000, 0.000000000000000000 ) ) ;
#72022=CARTESIAN_POINT ( 'NONE',  ( -3.469446951953614189E-15, 3.500000000000003109, 2.602085213965210642E-15 ) ) ;
#72140=VECTOR ( 'NONE', #148252, 1000.000000000000000 ) ;
#72191=CARTESIAN_POINT ( 'NONE',  ( 4.627371609795831357E-16, 2.099999999999997868, -2.600000000000008082 ) ) ;
#72193=ORIENTED_EDGE ( 'NONE', *, *, #168967, .F. ) ;
#72961=DIRECTION ( 'NONE',  ( 0.000000000000000000, -1.000000000000000000, 0.000000000000000000 ) ) ;
#73227=DIRECTION ( 'NONE',  ( -5.551115123125765446E-17, 0.000000000000000000, 1.000000000000000000 ) ) ;
#73390=AXIS2_PLACEMENT_3D ( 'NONE', #189709, #28283, #94378 ) ;
#73686=VERTEX_POINT ( 'NONE', #51084 ) ;
#73789=DIRECTION ( 'NONE',  ( 5.551115123125765446E-17, 0.000000000000000000, -1.000000000000000000 ) ) ;
#74357=VECTOR ( 'NONE', #165403, 1000.000000000000000 ) ;
#74614=AXIS2_PLACEMENT_3D ( 'NONE', #113987, #11057, #46803 ) ;
#75246=CARTESIAN_POINT ( 'NONE',  ( 0.000000000000000000, 4.500000000000003553, 0.000000000000000000 ) ) ;
#75587=CARTESIAN_POINT ( 'NONE',  ( 0.000000000000000000, 1.551257596039481879, 0.000000000000000000 ) ) ;
#75670=TOROIDAL_SURFACE ( 'NONE', #214011, 1.924999999999999822, 0.1000000000000000056 ) ;
#75757=CIRCLE ( 'NONE', #58443, 2.750000000000008438 ) ;
#75883=ORIENTED_EDGE ( 'NONE', *, *, #60288, .F. ) ;
#75904=CYLINDRICAL_SURFACE ( 'NONE', #189882, 3.000000000000010214 ) ;
#75964=ORIENTED_EDGE ( 'NONE', *, *, #18607, .T. ) ;
#76548=EDGE_CURVE ( 'NONE', #106, #132709, #56091, .T. ) ;
#76599=CARTESIAN_POINT ( 'NONE',  ( 1.249000902703297164E-16, 4.099999999999999645, -2.250000000000000000 ) ) ;
#77132=ORIENTED_EDGE ( 'NONE', *, *, #88561, .T. ) ;
#77394=EDGE_LOOP ( 'NONE', ( #19843, #195250 ) ) ;
#77536=VERTEX_POINT ( 'NONE', #65939 ) ;
#77777=DIRECTION ( 'NONE',  ( 0.000000000000000000, -1.000000000000000000, 0.000000000000000000 ) ) ;
#77913=EDGE_LOOP ( 'NONE', ( #58613, #144797, #49793, #162481 ) ) ;
#78012=ORIENTED_EDGE ( 'NONE', *, *, #178677, .F. ) ;
#78022=VECTOR ( 'NONE', #70635, 1000.000000000000000 ) ;
#78041=EDGE_CURVE ( 'NONE', #111689, #184764, #208508, .T. ) ;
#78316=VERTEX_POINT ( 'NONE', #163493 ) ;
#78493=VERTEX_POINT ( 'NONE', #188252 ) ;
#78944=CARTESIAN_POINT ( 'NONE',  ( 8.881784197001254049E-17, 3.599999999999999201, -1.600000000000005196 ) ) ;
#79411=ORIENTED_EDGE ( 'NONE', *, *, #31316, .F. ) ;
#79746=EDGE_LOOP ( 'NONE', ( #133195, #57979, #32776, #92293 ) ) ;
#79802=DIRECTION ( 'NONE',  ( -0.000000000000000000, 1.000000000000000000, -0.000000000000000000 ) ) ;
#79837=AXIS2_PLACEMENT_3D ( 'NONE', #30059, #13787, #129776 ) ;
#80082=DIRECTION ( 'NONE',  ( 0.000000000000000000, -1.000000000000000000, 0.000000000000000000 ) ) ;
#80513=DIRECTION ( 'NONE',  ( -1.000000000000000000, -0.000000000000000000, -5.551115123125765446E-17 ) ) ;
#80522=ORIENTED_EDGE ( 'NONE', *, *, #147028, .F. ) ;
#81014=CARTESIAN_POINT ( 'NONE',  ( 0.000000000000000000, 4.000000000000003553, 0.000000000000000000 ) ) ;
#81022=ORIENTED_EDGE ( 'NONE', *, *, #25737, .F. ) ;
#81090=DIRECTION ( 'NONE',  ( -1.000000000000000000, -0.000000000000000000, -5.551115123125765446E-17 ) ) ;
#81143=EDGE_LOOP ( 'NONE', ( #122265, #77132 ) ) ;
#81477=ORIENTED_EDGE ( 'NONE', *, *, #34501, .F. ) ;
#81925=AXIS2_PLACEMENT_3D ( 'NONE', #75587, #63599, #44166 ) ;
#82190=FACE_OUTER_BOUND ( 'NONE', #10105, .T. ) ;
#82668=EDGE_LOOP ( 'NONE', ( #75883, #148517, #43741, #3765 ) ) ;
#82749=DIRECTION ( 'NONE',  ( 1.000000000000000000, 0.000000000000000000, -6.695352868347765393E-17 ) ) ;
#83669=EDGE_CURVE ( 'NONE', #9073, #205992, #101519, .T. ) ;
#83957=ORIENTED_EDGE ( 'NONE', *, *, #127735, .F. ) ;
#83977=CIRCLE ( 'NONE', #142793, 2.500000000000007994 ) ;
#84029=AXIS2_PLACEMENT_3D ( 'NONE', #114159, #80513, #180152 ) ;
#84058=AXIS2_PLACEMENT_3D ( 'NONE', #109891, #143428, #175904 ) ;
#84153=DIRECTION ( 'NONE',  ( 0.000000000000000000, -1.000000000000000000, 0.000000000000000000 ) ) ;
#84155=CARTESIAN_POINT ( 'NONE',  ( -3.469446951953614189E-15, 3.500000000000003109, 2.602085213965210642E-15 ) ) ;
#84727=CARTESIAN_POINT ( 'NONE',  ( 0.000000000000000000, 2.000000000000001776, 0.000000000000000000 ) ) ;
#84959=EDGE_LOOP ( 'NONE', ( #31600, #121541 ) ) ;
#84966=AXIS2_PLACEMENT_3D ( 'NONE', #85525, #136434, #69252 ) ;
#85403=CIRCLE ( 'NONE', #19682, 1.600000000000005196 ) ;
#85525=CARTESIAN_POINT ( 'NONE',  ( 1.288855427156948835E-16, 3.400000000000000355, 1.925000000000005818 ) ) ;
#86344=EDGE_CURVE ( 'NONE', #195087, #201525, #43165, .T. ) ;
#86573=LINE ( 'NONE', #152636, #87132 ) ;
#86580=DIRECTION ( 'NONE',  ( -5.551115123125766062E-17, 0.000000000000000000, 1.000000000000000000 ) ) ;
#86838=ORIENTED_EDGE ( 'NONE', *, *, #78041, .F. ) ;
#87132=VECTOR ( 'NONE', #18358, 1000.000000000000114 ) ;
#87558=PLANE ( 'NONE',  #107733 ) ;
#87805=ORIENTED_EDGE ( 'NONE', *, *, #18607, .F. ) ;
#87810=EDGE_LOOP ( 'NONE', ( #210453, #94622, #4493, #87805 ) ) ;
#87922=CARTESIAN_POINT ( 'NONE',  ( 1.355808955840426748E-16, 3.500000000000003109, 2.025000000000006573 ) ) ;
#87955=VERTEX_POINT ( 'NONE', #101484 ) ;
#88045=PLANE ( 'NONE',  #96791 ) ;
#88406=CARTESIAN_POINT ( 'NONE',  ( 3.826480369638860602E-16, 4.400000000000001243, -2.150000000000006573 ) ) ;
#88412=PLANE ( 'NONE',  #126052 ) ;
#88561=EDGE_CURVE ( 'NONE', #165933, #168625, #147200, .T. ) ;
#88648=DIRECTION ( 'NONE',  ( 5.551115123125766062E-17, 0.000000000000000000, -1.000000000000000000 ) ) ;
#89009=DIRECTION ( 'NONE',  ( 0.000000000000000000, -1.000000000000000000, 0.000000000000000000 ) ) ;
#89054=TOROIDAL_SURFACE ( 'NONE', #51000, 2.149999999999999911, 0.1000000000000000056 ) ;
#89248=DIRECTION ( 'NONE',  ( -5.551115123125766062E-17, 0.000000000000000000, 1.000000000000000000 ) ) ;
#89520=DIRECTION ( 'NONE',  ( 0.000000000000000000, 1.000000000000000000, 0.000000000000000000 ) ) ;
#89622=EDGE_LOOP ( 'NONE', ( #37051, #31594, #126113, #42382 ) ) ;
#89635=( NAMED_UNIT ( * ) PLANE_ANGLE_UNIT ( ) SI_UNIT ( $, .RADIAN. ) );
#89711=CARTESIAN_POINT ( 'NONE',  ( 0.000000000000000000, 4.000000000000003553, 0.000000000000000000 ) ) ;
#89785=FACE_OUTER_BOUND ( 'NONE', #81143, .T. ) ;
#89960=CIRCLE ( 'NONE', #24200, 2.750000000000008438 ) ;
#90590=DIRECTION ( 'NONE',  ( -5.551115123125766062E-17, 0.000000000000000000, 1.000000000000000000 ) ) ;
#90704=SURFACE_SIDE_STYLE ('',( #105910 ) ) ;
#90882=CARTESIAN_POINT ( 'NONE',  ( 4.627371609795830371E-16, 1.999999999999999556, -2.600000000000008082 ) ) ;
#90966=ADVANCED_FACE ( 'NONE', ( #158504 ), #92467, .F. ) ;
#90975=DIRECTION ( 'NONE',  ( -0.000000000000000000, 1.000000000000000000, -0.000000000000000000 ) ) ;
#91003=EDGE_CURVE ( 'NONE', #142577, #150798, #62074, .T. ) ;
#91015=ORIENTED_EDGE ( 'NONE', *, *, #57465, .F. ) ;
#91061=AXIS2_PLACEMENT_3D ( 'NONE', #78944, #81090, #97364 ) ;
#91483=CARTESIAN_POINT ( 'NONE',  ( 0.000000000000000000, 3.466143782776612170, 0.000000000000000000 ) ) ;
#91642=DIRECTION ( 'NONE',  ( -5.551115123125765446E-17, 0.000000000000000000, 1.000000000000000000 ) ) ;
#91662=CIRCLE ( 'NONE', #195380, 0.09999999999999982514 ) ;
#91753=VERTEX_POINT ( 'NONE', #29021 ) ;
#91819=AXIS2_PLACEMENT_3D ( 'NONE', #81014, #143932, #197949 ) ;
#91960=EDGE_CURVE ( 'NONE', #206340, #174590, #185905, .T. ) ;
#91989=CARTESIAN_POINT ( 'NONE',  ( 0.000000000000000000, 3.466143782776612170, 0.000000000000000000 ) ) ;
#91996=CARTESIAN_POINT ( 'NONE',  ( -0.6170404364503407901, -1.000000000000000888, 1.902435570468869797 ) ) ;
#92035=EDGE_CURVE ( 'NONE', #36555, #182678, #52720, .T. ) ;
#92280=CARTESIAN_POINT ( 'NONE',  ( 1.347439764754987941E-16, 1.551257596039481879, 2.000000000000000000 ) ) ;
#92293=ORIENTED_EDGE ( 'NONE', *, *, #156185, .F. ) ;
#92464=CARTESIAN_POINT ( 'NONE',  ( 0.000000000000000000, 4.400000000000001243, 0.000000000000000000 ) ) ;
#92467=CYLINDRICAL_SURFACE ( 'NONE', #22368, 2.025000000000006573 ) ;
#92729=DIRECTION ( 'NONE',  ( 0.000000000000000000, 1.000000000000000000, 0.000000000000000000 ) ) ;
#92739=VERTEX_POINT ( 'NONE', #46605 ) ;
#92839=( NAMED_UNIT ( * ) SI_UNIT ( $, .STERADIAN. ) SOLID_ANGLE_UNIT ( ) );
#92866=AXIS2_PLACEMENT_3D ( 'NONE', #43237, #24815, #205697 ) ;
#93021=EDGE_CURVE ( 'NONE', #149924, #174590, #63997, .T. ) ;
#93323=( GEOMETRIC_REPRESENTATION_CONTEXT ( 3 ) GLOBAL_UNCERTAINTY_ASSIGNED_CONTEXT ( ( #150387 ) ) GLOBAL_UNIT_ASSIGNED_CONTEXT ( ( #171936, #89635, #139448 ) ) REPRESENTATION_CONTEXT ( 'NONE', 'WORKASPACE' ) );
#93378=EDGE_CURVE ( 'NONE', #168625, #165933, #46857, .T. ) ;
#93452=EDGE_CURVE ( 'NONE', #202678, #194213, #109222, .T. ) ;
#93852=PRODUCT ( 'isolation 510', 'isolation 510', '', ( #69877 ) ) ;
#94378=DIRECTION ( 'NONE',  ( 5.551115123125765446E-17, 0.000000000000000000, -1.000000000000000000 ) ) ;
#94619=CONICAL_SURFACE ( 'NONE', #1174, 2.000000000000006217, 0.01725463330310792257 ) ;
#94622=ORIENTED_EDGE ( 'NONE', *, *, #65245, .F. ) ;
#94745=DIRECTION ( 'NONE',  ( -5.551115123125766062E-17, 0.000000000000000000, 1.000000000000000000 ) ) ;
#94848=ORIENTED_EDGE ( 'NONE', *, *, #119633, .F. ) ;
#95181=DIRECTION ( 'NONE',  ( 0.000000000000000000, -1.000000000000000000, 0.000000000000000000 ) ) ;
#95216=CARTESIAN_POINT ( 'NONE',  ( 0.000000000000000000, 0.000000000000000000, 0.000000000000000000 ) ) ;
#95397=FACE_OUTER_BOUND ( 'NONE', #184303, .T. ) ;
#95461=DIRECTION ( 'NONE',  ( -5.551115123125764829E-17, 0.000000000000000000, 1.000000000000000000 ) ) ;
#95530=ORIENTED_EDGE ( 'NONE', *, *, #114707, .T. ) ;
#95592=CIRCLE ( 'NONE', #5680, 2.025000000000006573 ) ;
#95724=ADVANCED_FACE ( 'NONE', ( #138464 ), #126685, .F. ) ;
#95728=DIRECTION ( 'NONE',  ( 0.000000000000000000, -1.000000000000000000, 0.000000000000000000 ) ) ;
#95911=PRODUCT_DEFINITION ( 'UNKNOWN', '', #104116, #199818 ) ;
#95917=ORIENTED_EDGE ( 'NONE', *, *, #137329, .T. ) ;
#96367=CARTESIAN_POINT ( 'NONE',  ( 0.000000000000000000, 0.000000000000000000, 0.000000000000000000 ) ) ;
#96487=ORIENTED_EDGE ( 'NONE', *, *, #114707, .F. ) ;
#96650=ADVANCED_FACE ( 'NONE', ( #167284 ), #19939, .T. ) ;
#96713=CARTESIAN_POINT ( 'NONE',  ( 0.000000000000000000, 4.500000000000003553, 0.000000000000000000 ) ) ;
#96760=ORIENTED_EDGE ( 'NONE', *, *, #164952, .T. ) ;
#96791=AXIS2_PLACEMENT_3D ( 'NONE', #154116, #71763, #50214 ) ;
#97364=DIRECTION ( 'NONE',  ( -5.551115123125758667E-17, 0.000000000000000000, 1.000000000000000000 ) ) ;
#97562=EDGE_CURVE ( 'NONE', #194213, #29472, #60996, .T. ) ;
#97787=AXIS2_PLACEMENT_3D ( 'NONE', #153682, #42083, #57246 ) ;
#98586=DIRECTION ( 'NONE',  ( 0.000000000000000000, -1.000000000000000000, 0.000000000000000000 ) ) ;
#98599=TOROIDAL_SURFACE ( 'NONE', #43257, 1.924999999999999822, 0.1000000000000000056 ) ;
#98821=AXIS2_PLACEMENT_3D ( 'NONE', #164966, #148725, #143702 ) ;
#99488=AXIS2_PLACEMENT_3D ( 'NONE', #35220, #101296, #169499 ) ;
#99877=EDGE_LOOP ( 'NONE', ( #151631, #175064, #133247, #146838 ) ) ;
#100676=DIRECTION ( 'NONE',  ( 0.000000000000000000, -1.000000000000000000, 0.000000000000000000 ) ) ;
#100796=DIRECTION ( 'NONE',  ( -1.000000000000000000, 0.000000000000000000, -5.551115123125765446E-17 ) ) ;
#101296=DIRECTION ( 'NONE',  ( 0.000000000000000000, 1.000000000000000000, 0.000000000000000000 ) ) ;
#101347=CIRCLE ( 'NONE', #84029, 0.1000000000000000472 ) ;
#101403=DIRECTION ( 'NONE',  ( 5.551115123125764213E-17, 0.000000000000000000, -1.000000000000000000 ) ) ;
#101484=CARTESIAN_POINT ( 'NONE',  ( 1.004302930252164871E-16, 4.400000000000001243, 1.500000000000000222 ) ) ;
#101519=CIRCLE ( 'NONE', #63498, 3.000000000000010214 ) ;
#101653=LINE ( 'NONE', #18249, #180339 ) ;
#101781=CLOSED_SHELL ( 'NONE', ( #148919, #189311, #90966, #39481, #57658, #36169, #206348, #182303, #116512, #26308, #120033, #32992, #24949, #34930, #53647, #96650, #157529, #95724, #143463, #27472, #16348, #113298, #71547, #16562, #167322, #123897, #12395, #155788, #131203, #184348, #61624, #134784, #147965, #151618, #210185, #46402, #140206, #15092, #187801, #159622, #212994, #131789 ) ) ;
#101873=DIRECTION ( 'NONE',  ( 5.551115123125766062E-17, 0.000000000000000000, -1.000000000000000000 ) ) ;
#101898=VECTOR ( 'NONE', #175042, 1000.000000000000000 ) ;
#101999=VECTOR ( 'NONE', #197157, 1000.000000000000000 ) ;
#102202=AXIS2_PLACEMENT_3D ( 'NONE', #117864, #19213, #135136 ) ;
#102279=AXIS2_PLACEMENT_3D ( 'NONE', #66440, #20893, #115295 ) ;
#102297=CARTESIAN_POINT ( 'NONE',  ( 0.000000000000000000, 3.500000000000003109, 0.000000000000000000 ) ) ;
#102541=CARTESIAN_POINT ( 'NONE',  ( 1.506454395378251805E-16, 4.500000000000003553, 2.250000000000006661 ) ) ;
#102992=ORIENTED_EDGE ( 'NONE', *, *, #142604, .F. ) ;
#103212=VECTOR ( 'NONE', #105756, 1000.000000000000000 ) ;
#103625=PLANE ( 'NONE',  #148256 ) ;
#103726=EDGE_LOOP ( 'NONE', ( #10534, #81022, #208078, #108940 ) ) ;
#103772=LINE ( 'NONE', #169824, #72140 ) ;
#103812=DIRECTION ( 'NONE',  ( -5.551115123125765446E-17, 0.000000000000000000, 1.000000000000000000 ) ) ;
#103842=CARTESIAN_POINT ( 'NONE',  ( 0.000000000000000000, 3.500000000000003109, 0.000000000000000000 ) ) ;
#104081=AXIS2_PLACEMENT_3D ( 'NONE', #61085, #46989, #144515 ) ;
#104116=PRODUCT_DEFINITION_FORMATION_WITH_SPECIFIED_SOURCE ( 'ANY', '', #93852, .NOT_KNOWN. ) ;
#104138=DIRECTION ( 'NONE',  ( 0.000000000000000000, 1.000000000000000000, 0.000000000000000000 ) ) ;
#104577=CIRCLE ( 'NONE', #45838, 1.500000000000005107 ) ;
#104892=CIRCLE ( 'NONE', #149880, 2.025000000000006573 ) ;
#105092=VERTEX_POINT ( 'NONE', #124397 ) ;
#105269=DIRECTION ( 'NONE',  ( -5.551115123125764829E-17, 0.000000000000000000, 1.000000000000000000 ) ) ;
#105280=CARTESIAN_POINT ( 'NONE',  ( 1.506454395378247121E-16, 4.400000000000001243, 2.250000000000000000 ) ) ;
#105506=FACE_OUTER_BOUND ( 'NONE', #141659, .T. ) ;
#105535=ORIENTED_EDGE ( 'NONE', *, *, #105847, .T. ) ;
#105597=( LENGTH_UNIT ( ) NAMED_UNIT ( * ) SI_UNIT ( .MILLI., .METRE. ) );
#105756=DIRECTION ( 'NONE',  ( 0.000000000000000000, -1.000000000000000000, 0.000000000000000000 ) ) ;
#105847=EDGE_CURVE ( 'NONE', #106531, #92739, #47776, .T. ) ;
#105878=SURFACE_STYLE_FILL_AREA ( #122175 ) ;
#105900=CARTESIAN_POINT ( 'NONE',  ( 0.000000000000000000, -0.5000000000000004441, 0.000000000000000000 ) ) ;
#105910=SURFACE_STYLE_FILL_AREA ( #158883 ) ;
#105935=AXIS2_PLACEMENT_3D ( 'NONE', #119656, #51402, #37273 ) ;
#106141=DIRECTION ( 'NONE',  ( 0.000000000000000000, 1.000000000000000000, 0.000000000000000000 ) ) ;
#106531=VERTEX_POINT ( 'NONE', #76599 ) ;
#106602=ORIENTED_EDGE ( 'NONE', *, *, #190530, .T. ) ;
#106647=TOROIDAL_SURFACE ( 'NONE', #26953, 2.349999999999999645, 0.1000000000000000056 ) ;
#106669=CYLINDRICAL_SURFACE ( 'NONE', #84058, 2.500000000000007994 ) ;
#106870=STYLED_ITEM ( 'NONE', ( #129639 ), #13191 ) ;
#107037=VERTEX_POINT ( 'NONE', #12143 ) ;
#107219=CARTESIAN_POINT ( 'NONE',  ( 0.000000000000000000, 2.000000000000001776, 0.000000000000000000 ) ) ;
#107367=CARTESIAN_POINT ( 'NONE',  ( 1.506454395378247121E-16, 4.099999999999999645, 2.250000000000000000 ) ) ;
#107693=VECTOR ( 'NONE', #89009, 1000.000000000000000 ) ;
#107733=AXIS2_PLACEMENT_3D ( 'NONE', #89711, #7345, #103812 ) ;
#107994=ORIENTED_EDGE ( 'NONE', *, *, #39268, .F. ) ;
#108039=SURFACE_STYLE_USAGE ( .BOTH. , #171902 ) ;
#108165=FACE_OUTER_BOUND ( 'NONE', #30748, .T. ) ;
#108346=CYLINDRICAL_SURFACE ( 'NONE', #45681, 1.500000000000005107 ) ;
#108427=CIRCLE ( 'NONE', #91061, 0.1000000000000000472 ) ;
#108556=CIRCLE ( 'NONE', #32419, 2.250000000000006661 ) ;
#108849=ORIENTED_EDGE ( 'NONE', *, *, #156185, .T. ) ;
#108940=ORIENTED_EDGE ( 'NONE', *, *, #137329, .F. ) ;
#109024=CARTESIAN_POINT ( 'NONE',  ( 0.000000000000000000, 4.000000000000003553, 0.000000000000000000 ) ) ;
#109222=CIRCLE ( 'NONE', #198933, 2.000000000000006217 ) ;
#109243=EDGE_CURVE ( 'NONE', #111689, #205992, #49473, .T. ) ;
#109450=AXIS2_PLACEMENT_3D ( 'NONE', #204010, #55657, #186717 ) ;
#109549=CARTESIAN_POINT ( 'NONE',  ( 0.000000000000000000, -0.5000000000000004441, 0.000000000000000000 ) ) ;
#109735=CARTESIAN_POINT ( 'NONE',  ( 0.000000000000000000, 1.899999999999999023, 0.000000000000000000 ) ) ;
#109761=AXIS2_PLACEMENT_3D ( 'NONE', #160173, #141836, #60530 ) ;
#109891=CARTESIAN_POINT ( 'NONE',  ( 0.000000000000000000, 4.000000000000003553, 0.000000000000000000 ) ) ;
#110415=DIRECTION ( 'NONE',  ( -1.000000000000000000, 0.000000000000000000, -5.551115123125765446E-17 ) ) ;
#110431=( GEOMETRIC_REPRESENTATION_CONTEXT ( 3 ) GLOBAL_UNCERTAINTY_ASSIGNED_CONTEXT ( ( #34205 ) ) GLOBAL_UNIT_ASSIGNED_CONTEXT ( ( #105597, #120830, #20031 ) ) REPRESENTATION_CONTEXT ( 'NONE', 'WORKASPACE' ) );
#110593=AXIS2_PLACEMENT_3D ( 'NONE', #139314, #176075, #91642 ) ;
#110678=CARTESIAN_POINT ( 'NONE',  ( 0.000000000000000000, 4.099999999999999645, 0.000000000000000000 ) ) ;
#111254=ORIENTED_EDGE ( 'NONE', *, *, #157474, .T. ) ;
#111294=ORIENTED_EDGE ( 'NONE', *, *, #200849, .T. ) ;
#111570=DIRECTION ( 'NONE',  ( 0.000000000000000000, 1.000000000000000000, 0.000000000000000000 ) ) ;
#111590=ORIENTED_EDGE ( 'NONE', *, *, #83669, .T. ) ;
#111689=VERTEX_POINT ( 'NONE', #191591 ) ;
#112023=CARTESIAN_POINT ( 'NONE',  ( 0.000000000000000000, 3.466143782776612170, 0.000000000000000000 ) ) ;
#112288=CARTESIAN_POINT ( 'NONE',  ( 0.000000000000000000, 1.551257596039481879, 0.000000000000000000 ) ) ;
#112662=ORIENTED_EDGE ( 'NONE', *, *, #150919, .F. ) ;
#112788=AXIS2_PLACEMENT_3D ( 'NONE', #207396, #26509, #94745 ) ;
#112907=DIRECTION ( 'NONE',  ( -5.551115123125764829E-17, 0.000000000000000000, 1.000000000000000000 ) ) ;
#113298=ADVANCED_FACE ( 'NONE', ( #6947 ), #106669, .T. ) ;
#113332=CARTESIAN_POINT ( 'NONE',  ( 0.000000000000000000, 3.400000000000000355, 0.000000000000000000 ) ) ;
#113400=AXIS2_PLACEMENT_3D ( 'NONE', #59537, #9723, #146158 ) ;
#113617=CIRCLE ( 'NONE', #92866, 2.025000000000006573 ) ;
#113904=ORIENTED_EDGE ( 'NONE', *, *, #42520, .T. ) ;
#113987=CARTESIAN_POINT ( 'NONE',  ( 0.000000000000000000, -0.5000000000000004441, 0.000000000000000000 ) ) ;
#114159=CARTESIAN_POINT ( 'NONE',  ( 1.068589661201713072E-16, 3.400000000000000355, -1.925000000000005818 ) ) ;
#114697=ORIENTED_EDGE ( 'NONE', *, *, #93021, .T. ) ;
#114707=EDGE_CURVE ( 'NONE', #106531, #182678, #108556, .T. ) ;
#114767=CARTESIAN_POINT ( 'NONE',  ( 0.000000000000000000, 1.551257596039481879, 0.000000000000000000 ) ) ;
#114870=CARTESIAN_POINT ( 'NONE',  ( 0.000000000000000000, 4.400000000000001243, 0.000000000000000000 ) ) ;
#114874=ORIENTED_EDGE ( 'NONE', *, *, #133578, .T. ) ;
#114891=CARTESIAN_POINT ( 'NONE',  ( 3.915468285211845848E-16, 4.500000000000003553, -2.149999999999999911 ) ) ;
#115295=DIRECTION ( 'NONE',  ( -5.551115123125766062E-17, 0.000000000000000000, 1.000000000000000000 ) ) ;
#115310=EDGE_CURVE ( 'NONE', #206340, #78493, #195070, .T. ) ;
#115422=CYLINDRICAL_SURFACE ( 'NONE', #117581, 2.025000000000006573 ) ;
#115620=CARTESIAN_POINT ( 'NONE',  ( 0.000000000000000000, 3.900000000000000799, 0.000000000000000000 ) ) ;
#115732=FILL_AREA_STYLE_COLOUR ( '', #3487 ) ;
#115871=CIRCLE ( 'NONE', #102202, 0.09999999999999982514 ) ;
#115933=DIRECTION ( 'NONE',  ( -5.551115123125765446E-17, 0.000000000000000000, 1.000000000000000000 ) ) ;
#115942=CARTESIAN_POINT ( 'NONE',  ( 0.000000000000000000, 2.099999999999997868, 0.000000000000000000 ) ) ;
#116046=VERTEX_POINT ( 'NONE', #155965 ) ;
#116512=ADVANCED_FACE ( 'NONE', ( #60581 ), #188254, .T. ) ;
#116716=DIRECTION ( 'NONE',  ( 0.000000000000000000, -1.000000000000000000, 0.000000000000000000 ) ) ;
#117155=CARTESIAN_POINT ( 'NONE',  ( 1.387778780781441485E-16, 2.099999999999997868, -2.500000000000000000 ) ) ;
#117247=DIRECTION ( 'NONE',  ( 0.000000000000000000, -1.000000000000000000, 0.000000000000000000 ) ) ;
#117385=TOROIDAL_SURFACE ( 'NONE', #196796, 2.649999999999999911, 0.1000000000000000056 ) ;
#117534=CIRCLE ( 'NONE', #110593, 2.750000000000008438 ) ;
#117581=AXIS2_PLACEMENT_3D ( 'NONE', #102297, #182469, #15704 ) ;
#117783=EDGE_CURVE ( 'NONE', #78316, #29472, #150395, .T. ) ;
#117864=CARTESIAN_POINT ( 'NONE',  ( -1.193489751472043232E-16, 4.400000000000001243, 2.150000000000006573 ) ) ;
#118050=FACE_OUTER_BOUND ( 'NONE', #103726, .T. ) ;
#118089=AXIS2_PLACEMENT_3D ( 'NONE', #96367, #80082, #191686 ) ;
#118345=ORIENTED_EDGE ( 'NONE', *, *, #93378, .F. ) ;
#118947=DIRECTION ( 'NONE',  ( 5.551115123125765446E-17, 0.000000000000000000, -1.000000000000000000 ) ) ;
#119633=EDGE_CURVE ( 'NONE', #182678, #116046, #91662, .T. ) ;
#119656=CARTESIAN_POINT ( 'NONE',  ( 0.000000000000000000, 4.000000000000003553, 0.000000000000000000 ) ) ;
#119699=EDGE_LOOP ( 'NONE', ( #66579, #202620, #44058, #153061 ) ) ;
#119770=DIRECTION ( 'NONE',  ( 0.000000000000000000, -1.000000000000000000, 0.000000000000000000 ) ) ;
#119930=CARTESIAN_POINT ( 'NONE',  ( 1.673838217086946587E-16, 4.000000000000003553, 2.500000000000007994 ) ) ;
#120033=ADVANCED_FACE ( 'NONE', ( #136213 ), #53584, .T. ) ;
#120103=DIRECTION ( 'NONE',  ( -5.551115123125765446E-17, 0.000000000000000000, 1.000000000000000000 ) ) ;
#120830=( NAMED_UNIT ( * ) PLANE_ANGLE_UNIT ( ) SI_UNIT ( $, .RADIAN. ) );
#121051=STYLED_ITEM ( 'NONE', ( #22451 ), #194826 ) ;
#121056=DIRECTION ( 'NONE',  ( 1.000000000000000000, -0.000000000000000000, 1.779758311459929752E-16 ) ) ;
#121346=ORIENTED_EDGE ( 'NONE', *, *, #70880, .F. ) ;
#121388=VERTEX_POINT ( 'NONE', #132812 ) ;
#121523=EDGE_LOOP ( 'NONE', ( #18254, #38632, #161534, #168711 ) ) ;
#121541=ORIENTED_EDGE ( 'NONE', *, *, #62145, .T. ) ;
#121563=DIRECTION ( 'NONE',  ( -5.551115123125765446E-17, 0.000000000000000000, 1.000000000000000000 ) ) ;
#122083=ORIENTED_EDGE ( 'NONE', *, *, #168967, .T. ) ;
#122175=FILL_AREA_STYLE ('',( #115732 ) ) ;
#122192=EDGE_CURVE ( 'NONE', #73686, #77536, #57298, .T. ) ;
#122259=DIRECTION ( 'NONE',  ( 0.000000000000000000, 1.000000000000000000, 0.000000000000000000 ) ) ;
#122265=ORIENTED_EDGE ( 'NONE', *, *, #93378, .T. ) ;
#122355=DIRECTION ( 'NONE',  ( 0.000000000000000000, 1.000000000000000000, 0.000000000000000000 ) ) ;
#122835=CIRCLE ( 'NONE', #129619, 2.000000000000006217 ) ;
#122899=FACE_OUTER_BOUND ( 'NONE', #34699, .T. ) ;
#123084=EDGE_CURVE ( 'NONE', #57555, #121388, #192259, .T. ) ;
#123387=CARTESIAN_POINT ( 'NONE',  ( -8.881784197001254049E-17, 4.500000000000002665, 1.600000000000005196 ) ) ;
#123748=FACE_OUTER_BOUND ( 'NONE', #9712, .T. ) ;
#123838=ORIENTED_EDGE ( 'NONE', *, *, #12024, .T. ) ;
#123846=ORIENTED_EDGE ( 'NONE', *, *, #93021, .F. ) ;
#123897=ADVANCED_FACE ( 'NONE', ( #142176 ), #130240, .T. ) ;
#124397=CARTESIAN_POINT ( 'NONE',  ( 0.6170404364503330186, 3.466143782776612170, -1.902435570468861137 ) ) ;
#124895=CARTESIAN_POINT ( 'NONE',  ( -1.665334536937729880E-16, 0.000000000000000000, 3.000000000000000444 ) ) ;
#125671=AXIS2_PLACEMENT_3D ( 'NONE', #16232, #98586, #149461 ) ;
#125770=AXIS2_PLACEMENT_3D ( 'NONE', #91483, #22146, #153252 ) ;
#125829=CARTESIAN_POINT ( 'NONE',  ( 0.000000000000000000, 1.551257596039481879, 0.000000000000000000 ) ) ;
#126042=AXIS2_PLACEMENT_3D ( 'NONE', #68277, #100796, #186306 ) ;
#126052=AXIS2_PLACEMENT_3D ( 'NONE', #6058, #135042, #183763 ) ;
#126113=ORIENTED_EDGE ( 'NONE', *, *, #167075, .F. ) ;
#126241=VECTOR ( 'NONE', #128231, 1000.000000000000000 ) ;
#126455=DIRECTION ( 'NONE',  ( 5.551115123125764213E-17, 0.000000000000000000, -1.000000000000000000 ) ) ;
#126685=CONICAL_SURFACE ( 'NONE', #202649, 1.903066852858540603, 0.4537856055185301996 ) ;
#127421=DIRECTION ( 'NONE',  ( 0.000000000000000000, 1.000000000000000000, 0.000000000000000000 ) ) ;
#127695=CARTESIAN_POINT ( 'NONE',  ( 0.000000000000000000, 2.000000000000001776, 0.000000000000000000 ) ) ;
#127735=EDGE_CURVE ( 'NONE', #87955, #166237, #64559, .T. ) ;
#127991=VECTOR ( 'NONE', #182433, 1000.000000000000114 ) ;
#128047=DIRECTION ( 'NONE',  ( -5.551115123125766062E-17, 0.000000000000000000, 1.000000000000000000 ) ) ;
#128112=EDGE_LOOP ( 'NONE', ( #202594, #157792, #159167, #111590 ) ) ;
#128163=ORIENTED_EDGE ( 'NONE', *, *, #62788, .T. ) ;
#128231=DIRECTION ( 'NONE',  ( 0.000000000000000000, -1.000000000000000000, 0.000000000000000000 ) ) ;
#129299=ORIENTED_EDGE ( 'NONE', *, *, #186296, .F. ) ;
#129619=AXIS2_PLACEMENT_3D ( 'NONE', #91989, #95181, #161230 ) ;
#129639=PRESENTATION_STYLE_ASSIGNMENT (( #108039 ) ) ;
#129716=CARTESIAN_POINT ( 'NONE',  ( 0.000000000000000000, 3.500000000000003109, 0.000000000000000000 ) ) ;
#129747=CARTESIAN_POINT ( 'NONE',  ( 5.339274934379806019E-16, -0.5000000000000004441, -3.000000000000010214 ) ) ;
#129776=DIRECTION ( 'NONE',  ( -5.551115123125765446E-17, 0.000000000000000000, 1.000000000000000000 ) ) ;
#129777=AXIS2_PLACEMENT_3D ( 'NONE', #25161, #157322, #9977 ) ;
#129793=VECTOR ( 'NONE', #84153, 1000.000000000000000 ) ;
#129901=ORIENTED_EDGE ( 'NONE', *, *, #9913, .F. ) ;
#129913=ORIENTED_EDGE ( 'NONE', *, *, #18291, .T. ) ;
#129933=AXIS2_PLACEMENT_3D ( 'NONE', #133500, #5551, #121563 ) ;
#129966=CIRCLE ( 'NONE', #98821, 2.650000000000008349 ) ;
#130240=CYLINDRICAL_SURFACE ( 'NONE', #74614, 3.000000000000010214 ) ;
#130860=DIRECTION ( 'NONE',  ( 0.000000000000000000, -1.000000000000000000, 0.000000000000000000 ) ) ;
#131203=ADVANCED_FACE ( 'NONE', ( #154886 ), #6470, .F. ) ;
#131422=EDGE_CURVE ( 'NONE', #136049, #147669, #108427, .T. ) ;
#131789=ADVANCED_FACE ( 'NONE', ( #82190 ), #94619, .F. ) ;
#131850=DIRECTION ( 'NONE',  ( 0.000000000000000000, 1.000000000000000000, 0.000000000000000000 ) ) ;
#131859=DIRECTION ( 'NONE',  ( -0.000000000000000000, -1.000000000000000000, -0.000000000000000000 ) ) ;
#132002=DIRECTION ( 'NONE',  ( 0.000000000000000000, 0.000000000000000000, 1.000000000000000000 ) ) ;
#132029=DIRECTION ( 'NONE',  ( 0.000000000000000000, 1.000000000000000000, 0.000000000000000000 ) ) ;
#132055=DIRECTION ( 'NONE',  ( 0.000000000000000000, -1.000000000000000000, 0.000000000000000000 ) ) ;
#132175=FACE_OUTER_BOUND ( 'NONE', #167289, .T. ) ;
#132658=AXIS2_PLACEMENT_3D ( 'NONE', #30215, #14997, #179669 ) ;
#132709=VERTEX_POINT ( 'NONE', #186160 ) ;
#132812=CARTESIAN_POINT ( 'NONE',  ( 2.847613298335896675E-16, 4.500000000000002665, -1.600000000000005196 ) ) ;
#133195=ORIENTED_EDGE ( 'NONE', *, *, #64213, .F. ) ;
#133247=ORIENTED_EDGE ( 'NONE', *, *, #17877, .T. ) ;
#133285=DIRECTION ( 'NONE',  ( -0.000000000000000000, -1.000000000000000000, -0.000000000000000000 ) ) ;
#133500=CARTESIAN_POINT ( 'NONE',  ( 0.000000000000000000, 4.500000000000003553, 0.000000000000000000 ) ) ;
#133578=EDGE_CURVE ( 'NONE', #121388, #166237, #201857, .T. ) ;
#133609=CIRCLE ( 'NONE', #178733, 2.025000000000006573 ) ;
#133856=AXIS2_PLACEMENT_3D ( 'NONE', #187388, #27014, #22734 ) ;
#133988=DIRECTION ( 'NONE',  ( -0.000000000000000000, -1.000000000000000000, -0.000000000000000000 ) ) ;
#134042=FACE_OUTER_BOUND ( 'NONE', #141916, .T. ) ;
#134327=CARTESIAN_POINT ( 'NONE',  ( -1.193489751472043232E-16, 4.500000000000003553, 2.150000000000006573 ) ) ;
#134397=AXIS2_PLACEMENT_3D ( 'NONE', #142768, #27910, #160046 ) ;
#134531=DIRECTION ( 'NONE',  ( -5.551115123125765446E-17, 0.000000000000000000, 1.000000000000000000 ) ) ;
#134636=EDGE_LOOP ( 'NONE', ( #186194, #139505, #148752, #114697 ) ) ;
#134784=ADVANCED_FACE ( 'NONE', ( #123748 ), #135722, .T. ) ;
#135042=DIRECTION ( 'NONE',  ( 0.000000000000000000, -1.000000000000000000, 0.000000000000000000 ) ) ;
#135136=DIRECTION ( 'NONE',  ( -5.551115123125782702E-17, 0.000000000000000000, 1.000000000000000000 ) ) ;
#135246=DIRECTION ( 'NONE',  ( 0.000000000000000000, -1.000000000000000000, 0.000000000000000000 ) ) ;
#135616=CARTESIAN_POINT ( 'NONE',  ( 2.847613298335896675E-16, 4.400000000000001243, -1.600000000000005196 ) ) ;
#135722=TOROIDAL_SURFACE ( 'NONE', #73390, 1.600000000000000311, 0.1000000000000000056 ) ;
#136049=VERTEX_POINT ( 'NONE', #42161 ) ;
#136213=FACE_OUTER_BOUND ( 'NONE', #119699, .T. ) ;
#136434=DIRECTION ( 'NONE',  ( 1.000000000000000000, 0.000000000000000000, -6.695352868347765393E-17 ) ) ;
#136539=ORIENTED_EDGE ( 'NONE', *, *, #1866, .F. ) ;
#136548=CIRCLE ( 'NONE', #146921, 2.400000000000007461 ) ;
#136726=CARTESIAN_POINT ( 'NONE',  ( 0.000000000000000000, 2.999999999999975131, 0.000000000000000000 ) ) ;
#136835=EDGE_CURVE ( 'NONE', #36555, #168625, #115871, .T. ) ;
#137057=AXIS2_PLACEMENT_3D ( 'NONE', #92464, #187781, #89248 ) ;
#137329=EDGE_CURVE ( 'NONE', #201525, #147150, #129966, .T. ) ;
#137417=DIRECTION ( 'NONE',  ( 0.000000000000000000, -1.000000000000000000, 0.000000000000000000 ) ) ;
#137420=DIRECTION ( 'NONE',  ( -5.551115123125766062E-17, 0.000000000000000000, 1.000000000000000000 ) ) ;
#138267=ORIENTED_EDGE ( 'NONE', *, *, #93452, .T. ) ;
#138405=ORIENTED_EDGE ( 'NONE', *, *, #65245, .T. ) ;
#138464=FACE_OUTER_BOUND ( 'NONE', #206267, .T. ) ;
#139027=AXIS2_PLACEMENT_3D ( 'NONE', #113332, #46147, #162022 ) ;
#139199=DIRECTION ( 'NONE',  ( 0.000000000000000000, -1.000000000000000000, 0.000000000000000000 ) ) ;
#139299=DIRECTION ( 'NONE',  ( 1.000000000000000000, -0.000000000000000000, 1.779758311459929752E-16 ) ) ;
#139314=CARTESIAN_POINT ( 'NONE',  ( 0.000000000000000000, 0.000000000000000000, 0.000000000000000000 ) ) ;
#139439=CARTESIAN_POINT ( 'NONE',  ( 1.841222038795635206E-16, 1.899999999999999023, 2.750000000000000000 ) ) ;
#139448=( NAMED_UNIT ( * ) SI_UNIT ( $, .STERADIAN. ) SOLID_ANGLE_UNIT ( ) );
#139505=ORIENTED_EDGE ( 'NONE', *, *, #39637, .T. ) ;
#140206=ADVANCED_FACE ( 'NONE', ( #12384 ), #206090, .F. ) ;
#140863=EDGE_LOOP ( 'NONE', ( #128163, #206431, #166464, #42683 ) ) ;
#140877=VERTEX_POINT ( 'NONE', #58650 ) ;
#141659=EDGE_LOOP ( 'NONE', ( #149677, #63823, #153791, #95530 ) ) ;
#141836=DIRECTION ( 'NONE',  ( 0.000000000000000000, -1.000000000000000000, 0.000000000000000000 ) ) ;
#141916=EDGE_LOOP ( 'NONE', ( #143809, #34880, #202971, #111254, #162784 ) ) ;
#141945=EDGE_CURVE ( 'NONE', #170139, #181670, #64475, .T. ) ;
#142176=FACE_OUTER_BOUND ( 'NONE', #128112, .T. ) ;
#142438=ORIENTED_EDGE ( 'NONE', *, *, #186296, .T. ) ;
#142577=VERTEX_POINT ( 'NONE', #139439 ) ;
#142604=EDGE_CURVE ( 'NONE', #145077, #91753, #95592, .T. ) ;
#142716=CARTESIAN_POINT ( 'NONE',  ( 1.387778780781445676E-16, 4.000000000000003553, -2.500000000000007994 ) ) ;
#142768=CARTESIAN_POINT ( 'NONE',  ( 0.000000000000000000, 2.000000000000001776, 0.000000000000000000 ) ) ;
#142793=AXIS2_PLACEMENT_3D ( 'NONE', #3245, #68250, #202515 ) ;
#142805=SHAPE_REPRESENTATION ( 'isolation 510', ( #200407 ), #13801 ) ;
#142810=FACE_BOUND ( 'NONE', #48835, .T. ) ;
#142991=ORIENTED_EDGE ( 'NONE', *, *, #26695, .F. ) ;
#143182=DIRECTION ( 'NONE',  ( 0.000000000000000000, 1.000000000000000000, 0.000000000000000000 ) ) ;
#143428=DIRECTION ( 'NONE',  ( 0.000000000000000000, -1.000000000000000000, 0.000000000000000000 ) ) ;
#143463=ADVANCED_FACE ( 'NONE', ( #17912 ), #168366, .F. ) ;
#143702=DIRECTION ( 'NONE',  ( -5.551115123125764829E-17, 0.000000000000000000, 1.000000000000000000 ) ) ;
#143809=ORIENTED_EDGE ( 'NONE', *, *, #156015, .F. ) ;
#143932=DIRECTION ( 'NONE',  ( -0.000000000000000000, -1.000000000000000000, -0.000000000000000000 ) ) ;
#143990=AXIS2_PLACEMENT_3D ( 'NONE', #39008, #90975, #171131 ) ;
#144515=DIRECTION ( 'NONE',  ( -5.551115123125758667E-17, 0.000000000000000000, 1.000000000000000000 ) ) ;
#144773=AXIS2_PLACEMENT_3D ( 'NONE', #195749, #163254, #182672 ) ;
#144797=ORIENTED_EDGE ( 'NONE', *, *, #200849, .F. ) ;
#145063=VECTOR ( 'NONE', #194649, 1000.000000000000000 ) ;
#145077=VERTEX_POINT ( 'NONE', #152722 ) ;
#145894=AXIS2_PLACEMENT_3D ( 'NONE', #19322, #34512, #35573 ) ;
#146158=DIRECTION ( 'NONE',  ( -5.551115123125765446E-17, 0.000000000000000000, 1.000000000000000000 ) ) ;
#146185=AXIS2_PLACEMENT_3D ( 'NONE', #72022, #139199, #40640 ) ;
#146253=VERTEX_POINT ( 'NONE', #166593 ) ;
#146516=AXIS2_PLACEMENT_3D ( 'NONE', #129716, #79802, #162141 ) ;
#146838=ORIENTED_EDGE ( 'NONE', *, *, #60529, .F. ) ;
#146863=CIRCLE ( 'NONE', #174545, 0.09999999999999982514 ) ;
#146895=CARTESIAN_POINT ( 'NONE',  ( 5.339274934379788269E-16, 0.000000000000000000, -3.000000000000000444 ) ) ;
#146921=AXIS2_PLACEMENT_3D ( 'NONE', #109024, #92729, #90590 ) ;
#147028=EDGE_CURVE ( 'NONE', #157913, #150798, #206699, .T. ) ;
#147084=DIRECTION ( 'NONE',  ( 1.779758311459929505E-16, 0.000000000000000000, -1.000000000000000000 ) ) ;
#147150=VERTEX_POINT ( 'NONE', #42253 ) ;
#147200=CIRCLE ( 'NONE', #64175, 2.150000000000006573 ) ;
#147301=ORIENTED_EDGE ( 'NONE', *, *, #147396, .T. ) ;
#147318=DIRECTION ( 'NONE',  ( 5.551115123125765446E-17, 0.000000000000000000, -1.000000000000000000 ) ) ;
#147396=EDGE_CURVE ( 'NONE', #91753, #145077, #133609, .T. ) ;
#147669=VERTEX_POINT ( 'NONE', #50758 ) ;
#147965=ADVANCED_FACE ( 'NONE', ( #168776 ), #151056, .T. ) ;
#148252=DIRECTION ( 'NONE',  ( 0.000000000000000000, -1.000000000000000000, 0.000000000000000000 ) ) ;
#148256=AXIS2_PLACEMENT_3D ( 'NONE', #169677, #116716, #154508 ) ;
#148307=AXIS2_PLACEMENT_3D ( 'NONE', #88406, #139299, #205328 ) ;
#148517=ORIENTED_EDGE ( 'NONE', *, *, #60529, .T. ) ;
#148725=DIRECTION ( 'NONE',  ( 0.000000000000000000, 1.000000000000000000, 0.000000000000000000 ) ) ;
#148752=ORIENTED_EDGE ( 'NONE', *, *, #1852, .T. ) ;
#148919=ADVANCED_FACE ( 'NONE', ( #59330 ), #199417, .F. ) ;
#149086=DIRECTION ( 'NONE',  ( -0.000000000000000000, 1.000000000000000000, -0.000000000000000000 ) ) ;
#149417=CARTESIAN_POINT ( 'NONE',  ( 0.000000000000000000, 1.899999999999999023, 0.000000000000000000 ) ) ;
#149461=DIRECTION ( 'NONE',  ( 5.551115123125764829E-17, 0.000000000000000000, -1.000000000000000000 ) ) ;
#149677=ORIENTED_EDGE ( 'NONE', *, *, #92035, .F. ) ;
#149880=AXIS2_PLACEMENT_3D ( 'NONE', #166404, #149086, #101403 ) ;
#149924=VERTEX_POINT ( 'NONE', #117155 ) ;
#150387=UNCERTAINTY_MEASURE_WITH_UNIT (LENGTH_MEASURE( 1.000000000000000082E-05 ), #171936, 'distance_accuracy_value', 'NONE');
#150395=CIRCLE ( 'NONE', #60393, 2.025000000000006573 ) ;
#150798=VERTEX_POINT ( 'NONE', #203949 ) ;
#150858=AXIS2_PLACEMENT_3D ( 'NONE', #112288, #178304, #162049 ) ;
#150919=EDGE_CURVE ( 'NONE', #142577, #147150, #16499, .T. ) ;
#151056=TOROIDAL_SURFACE ( 'NONE', #182103, 1.600000000000000311, 0.1000000000000000056 ) ;
#151333=CARTESIAN_POINT ( 'NONE',  ( -3.469446951953614189E-15, -1.000000000000000888, 2.602085213965210642E-15 ) ) ;
#151346=DIRECTION ( 'NONE',  ( 1.000000000000000000, -0.000000000000000000, 1.779758311459929752E-16 ) ) ;
#151395=DIRECTION ( 'NONE',  ( 0.000000000000000000, -1.000000000000000000, 0.000000000000000000 ) ) ;
#151554=AXIS2_PLACEMENT_3D ( 'NONE', #23409, #89520, #73227 ) ;
#151618=ADVANCED_FACE ( 'NONE', ( #204798 ), #89054, .T. ) ;
#151631=ORIENTED_EDGE ( 'NONE', *, *, #159020, .F. ) ;
#152039=CARTESIAN_POINT ( 'NONE',  ( -1.471045507628332367E-16, 1.899999999999999023, 2.650000000000008349 ) ) ;
#152391=DIRECTION ( 'NONE',  ( 0.000000000000000000, 1.000000000000000000, 0.000000000000000000 ) ) ;
#152509=AXIS2_PLACEMENT_3D ( 'NONE', #23641, #25775, #137420 ) ;
#152636=CARTESIAN_POINT ( 'NONE',  ( -1.110223024625156540E-16, 1.551257596039481879, 2.000000000000006217 ) ) ;
#152722=CARTESIAN_POINT ( 'NONE',  ( 1.124100812432970948E-16, -0.5000000000000004441, -2.025000000000006573 ) ) ;
#153003=CIRCLE ( 'NONE', #56069, 1.500000000000005107 ) ;
#153061=ORIENTED_EDGE ( 'NONE', *, *, #131422, .F. ) ;
#153252=DIRECTION ( 'NONE',  ( 5.551115123125765446E-17, 0.000000000000000000, -1.000000000000000000 ) ) ;
#153433=VECTOR ( 'NONE', #208725, 1000.000000000000000 ) ;
#153477=DIRECTION ( 'NONE',  ( 0.000000000000000000, 1.000000000000000000, 0.000000000000000000 ) ) ;
#153682=CARTESIAN_POINT ( 'NONE',  ( 4.271419947503845012E-16, 3.900000000000000799, -2.400000000000007461 ) ) ;
#153791=ORIENTED_EDGE ( 'NONE', *, *, #204906, .T. ) ;
#153996=LINE ( 'NONE', #87922, #41937 ) ;
#154063=ORIENTED_EDGE ( 'NONE', *, *, #62788, .F. ) ;
#154116=CARTESIAN_POINT ( 'NONE',  ( 0.000000000000000000, -0.5000000000000004441, 0.000000000000000000 ) ) ;
#154508=DIRECTION ( 'NONE',  ( 5.551115123125765446E-17, 0.000000000000000000, -1.000000000000000000 ) ) ;
#154681=CIRCLE ( 'NONE', #109761, 1.500000000000005107 ) ;
#154886=FACE_OUTER_BOUND ( 'NONE', #82668, .T. ) ;
#154897=ORIENTED_EDGE ( 'NONE', *, *, #88561, .F. ) ;
#155788=ADVANCED_FACE ( 'NONE', ( #3946, #70013 ), #103625, .F. ) ;
#155909=CARTESIAN_POINT ( 'NONE',  ( 1.387778780781441485E-16, 3.900000000000000799, -2.500000000000000000 ) ) ;
#155965=CARTESIAN_POINT ( 'NONE',  ( -1.304512053934558738E-16, 4.000000000000001776, 2.350000000000007194 ) ) ;
#156015=EDGE_CURVE ( 'NONE', #105092, #146253, #208561, .T. ) ;
#156185=EDGE_CURVE ( 'NONE', #168244, #78493, #136548, .T. ) ;
#156727=CIRCLE ( 'NONE', #191322, 2.000000000000006217 ) ;
#156766=SHAPE_REPRESENTATION_RELATIONSHIP ( 'NONE' , 'NONE' ,  #142805, #194826 ) ;
#156970=APPLICATION_CONTEXT ( 'automotive_design' ) ;
#157108=VECTOR ( 'NONE', #677, 1000.000000000000000 ) ;
#157113=CARTESIAN_POINT ( 'NONE',  ( 1.110223024625156540E-16, 1.551257596039481879, -2.000000000000006217 ) ) ;
#157227=AXIS2_PLACEMENT_3D ( 'NONE', #1087, #133285, #199292 ) ;
#157322=DIRECTION ( 'NONE',  ( 0.000000000000000000, 1.000000000000000000, 0.000000000000000000 ) ) ;
#157474=EDGE_CURVE ( 'NONE', #10457, #107037, #189468, .T. ) ;
#157529=ADVANCED_FACE ( 'NONE', ( #9642 ), #38959, .T. ) ;
#157792=ORIENTED_EDGE ( 'NONE', *, *, #54959, .F. ) ;
#157913=VERTEX_POINT ( 'NONE', #195867 ) ;
#157923=CARTESIAN_POINT ( 'NONE',  ( 0.000000000000000000, 1.750000000000001554, 0.000000000000000000 ) ) ;
#157965=ORIENTED_EDGE ( 'NONE', *, *, #10566, .F. ) ;
#158418=ORIENTED_EDGE ( 'NONE', *, *, #123084, .F. ) ;
#158504=FACE_OUTER_BOUND ( 'NONE', #207131, .T. ) ;
#158789=ORIENTED_EDGE ( 'NONE', *, *, #204906, .F. ) ;
#158883=FILL_AREA_STYLE ('',( #39802 ) ) ;
#159020=EDGE_CURVE ( 'NONE', #202678, #181670, #181380, .T. ) ;
#159056=ORIENTED_EDGE ( 'NONE', *, *, #39268, .T. ) ;
#159080=ORIENTED_EDGE ( 'NONE', *, *, #164952, .F. ) ;
#159167=ORIENTED_EDGE ( 'NONE', *, *, #53808, .T. ) ;
#159541=PRODUCT_DEFINITION_SHAPE ( 'NONE', 'NONE',  #95911 ) ;
#159565=DIRECTION ( 'NONE',  ( 5.551115123125764213E-17, 0.000000000000000000, -1.000000000000000000 ) ) ;
#159622=ADVANCED_FACE ( 'NONE', ( #64480 ), #115422, .F. ) ;
#159912=DIRECTION ( 'NONE',  ( 0.000000000000000000, -1.000000000000000000, 0.000000000000000000 ) ) ;
#160046=DIRECTION ( 'NONE',  ( -5.551115123125765446E-17, 0.000000000000000000, 1.000000000000000000 ) ) ;
#160173=CARTESIAN_POINT ( 'NONE',  ( 0.000000000000000000, 3.599999999999999201, 0.000000000000000000 ) ) ;
#160222=CIRCLE ( 'NONE', #125671, 3.000000000000010214 ) ;
#160700=DIRECTION ( 'NONE',  ( 5.551115123125765446E-17, 0.000000000000000000, -1.000000000000000000 ) ) ;
#160985=DIRECTION ( 'NONE',  ( 5.551115123125764829E-17, 0.000000000000000000, -1.000000000000000000 ) ) ;
#161171=FACE_OUTER_BOUND ( 'NONE', #57544, .T. ) ;
#161177=ORIENTED_EDGE ( 'NONE', *, *, #31468, .F. ) ;
#161230=DIRECTION ( 'NONE',  ( 5.551115123125765446E-17, 0.000000000000000000, -1.000000000000000000 ) ) ;
#161266=DIRECTION ( 'NONE',  ( 1.000000000000000000, 0.000000000000000000, 0.000000000000000000 ) ) ;
#161510=DIRECTION ( 'NONE',  ( 0.000000000000000000, 1.000000000000000000, 0.000000000000000000 ) ) ;
#161534=ORIENTED_EDGE ( 'NONE', *, *, #188635, .T. ) ;
#161660=DIRECTION ( 'NONE',  ( 0.000000000000000000, -1.000000000000000000, 0.000000000000000000 ) ) ;
#161900=ORIENTED_EDGE ( 'NONE', *, *, #55350, .T. ) ;
#162022=DIRECTION ( 'NONE',  ( 5.551115123125764213E-17, 0.000000000000000000, -1.000000000000000000 ) ) ;
#162049=DIRECTION ( 'NONE',  ( 5.551115123125765446E-17, 0.000000000000000000, -1.000000000000000000 ) ) ;
#162085=ORIENTED_EDGE ( 'NONE', *, *, #60288, .T. ) ;
#162141=DIRECTION ( 'NONE',  ( 5.551115123125766062E-17, 0.000000000000000000, -1.000000000000000000 ) ) ;
#162481=ORIENTED_EDGE ( 'NONE', *, *, #180453, .F. ) ;
#162784=ORIENTED_EDGE ( 'NONE', *, *, #62145, .F. ) ;
#162949=EDGE_CURVE ( 'NONE', #57555, #87955, #52128, .T. ) ;
#163254=DIRECTION ( 'NONE',  ( -0.000000000000000000, -1.000000000000000000, -0.000000000000000000 ) ) ;
#163493=CARTESIAN_POINT ( 'NONE',  ( 1.355808955840422310E-16, 2.999999999999975131, 2.024999999999999911 ) ) ;
#163758=ORIENTED_EDGE ( 'NONE', *, *, #122192, .T. ) ;
#164123=EDGE_LOOP ( 'NONE', ( #138267, #1, #166139, #142991 ) ) ;
#164952=EDGE_CURVE ( 'NONE', #77536, #78316, #153996, .T. ) ;
#164966=CARTESIAN_POINT ( 'NONE',  ( 0.000000000000000000, 2.000000000000001776, 0.000000000000000000 ) ) ;
#164968=AXIS2_PLACEMENT_3D ( 'NONE', #36307, #119770, #3781 ) ;
#165028=AXIS2_PLACEMENT_3D ( 'NONE', #207628, #176220, #175162 ) ;
#165187=EDGE_CURVE ( 'NONE', #195087, #157913, #54364, .T. ) ;
#165403=DIRECTION ( 'NONE',  ( 0.000000000000000000, -1.000000000000000000, 0.000000000000000000 ) ) ;
#165429=CIRCLE ( 'NONE', #134397, 2.600000000000008082 ) ;
#165666=DIRECTION ( 'NONE',  ( 0.000000000000000000, 1.000000000000000000, 0.000000000000000000 ) ) ;
#165766=TOROIDAL_SURFACE ( 'NONE', #207194, 2.600000000000000089, 0.1000000000000000056 ) ;
#165922=EDGE_LOOP ( 'NONE', ( #81477, #91015, #172915, #154897 ) ) ;
#165933=VERTEX_POINT ( 'NONE', #114891 ) ;
#165964=COLOUR_RGB ( '', 0.31764706, 0.68627451, 0.89019608) ;
#166139=ORIENTED_EDGE ( 'NONE', *, *, #117783, .F. ) ;
#166237=VERTEX_POINT ( 'NONE', #23708 ) ;
#166353=CIRCLE ( 'NONE', #194023, 2.000000000000006661 ) ;
#166404=CARTESIAN_POINT ( 'NONE',  ( 0.000000000000000000, 3.400000000000000355, 0.000000000000000000 ) ) ;
#166450=DIRECTION ( 'NONE',  ( -5.551115123125764829E-17, 0.000000000000000000, 1.000000000000000000 ) ) ;
#166464=ORIENTED_EDGE ( 'NONE', *, *, #19949, .T. ) ;
#166566=CIRCLE ( 'NONE', #145894, 2.025000000000006573 ) ;
#166593=CARTESIAN_POINT ( 'NONE',  ( 0.6170404364503319083, 3.500000000000003109, -1.902435570468858250 ) ) ;
#166621=ORIENTED_EDGE ( 'NONE', *, *, #147028, .T. ) ;
#166802=DIRECTION ( 'NONE',  ( 5.551115123125764829E-17, 0.000000000000000000, -1.000000000000000000 ) ) ;
#167075=EDGE_CURVE ( 'NONE', #78493, #168244, #21304, .T. ) ;
#167234=ORIENTED_EDGE ( 'NONE', *, *, #190530, .F. ) ;
#167284=FACE_OUTER_BOUND ( 'NONE', #54308, .T. ) ;
#167289=EDGE_LOOP ( 'NONE', ( #123846, #213612, #107994, #14905 ) ) ;
#167322=ADVANCED_FACE ( 'NONE', ( #142810, #89785 ), #58325, .T. ) ;
#167544=CARTESIAN_POINT ( 'NONE',  ( 1.124100812432971934E-16, 1.500000000000001332, -2.025000000000007905 ) ) ;
#168244=VERTEX_POINT ( 'NONE', #26124 ) ;
#168366=CONICAL_SURFACE ( 'NONE', #164968, 1.903066852858540603, 0.4537856055185301996 ) ;
#168377=ORIENTED_EDGE ( 'NONE', *, *, #141945, .T. ) ;
#168625=VERTEX_POINT ( 'NONE', #134327 ) ;
#168711=ORIENTED_EDGE ( 'NONE', *, *, #27074, .T. ) ;
#168776=FACE_OUTER_BOUND ( 'NONE', #17102, .T. ) ;
#168967=EDGE_CURVE ( 'NONE', #77536, #191870, #27829, .T. ) ;
#169297=ORIENTED_EDGE ( 'NONE', *, *, #12024, .F. ) ;
#169499=DIRECTION ( 'NONE',  ( -5.551115123125765446E-17, 0.000000000000000000, 1.000000000000000000 ) ) ;
#169677=CARTESIAN_POINT ( 'NONE',  ( 0.000000000000000000, 0.000000000000000000, 0.000000000000000000 ) ) ;
#169824=CARTESIAN_POINT ( 'NONE',  ( 1.004302930252168075E-16, 6.999999999999999112, 1.500000000000005107 ) ) ;
#169914=EDGE_CURVE ( 'NONE', #107037, #146253, #166353, .T. ) ;
#170117=ORIENTED_EDGE ( 'NONE', *, *, #91003, .T. ) ;
#170133=CARTESIAN_POINT ( 'NONE',  ( 1.071256458935645988E-16, 3.599999999999999201, 1.600000000000005196 ) ) ;
#170139=VERTEX_POINT ( 'NONE', #167544 ) ;
#170163=AXIS2_PLACEMENT_3D ( 'NONE', #127695, #130860, #47436 ) ;
#170715=FACE_BOUND ( 'NONE', #27774, .T. ) ;
#171131=DIRECTION ( 'NONE',  ( 5.551115123125764213E-17, 0.000000000000000000, -1.000000000000000000 ) ) ;
#171538=CARTESIAN_POINT ( 'NONE',  ( 0.000000000000000000, 4.500000000000003553, 0.000000000000000000 ) ) ;
#171709=CIRCLE ( 'NONE', #150858, 2.000000000000006217 ) ;
#171902=SURFACE_SIDE_STYLE ('',( #105878 ) ) ;
#171936=( LENGTH_UNIT ( ) NAMED_UNIT ( * ) SI_UNIT ( .MILLI., .METRE. ) );
#172221=CARTESIAN_POINT ( 'NONE',  ( 0.000000000000000000, 6.999999999999999112, 0.000000000000000000 ) ) ;
#172915=ORIENTED_EDGE ( 'NONE', *, *, #136835, .T. ) ;
#173101=DIRECTION ( 'NONE',  ( 0.000000000000000000, -1.000000000000000000, 0.000000000000000000 ) ) ;
#173176=DIRECTION ( 'NONE',  ( 5.551115123125764829E-17, 0.000000000000000000, -1.000000000000000000 ) ) ;
#173218=CARTESIAN_POINT ( 'NONE',  ( 1.071256458935646111E-16, 3.500000000000000888, 1.600000000000005196 ) ) ;
#173247=TOROIDAL_SURFACE ( 'NONE', #79837, 2.649999999999999911, 0.1000000000000000056 ) ;
#173294=DIRECTION ( 'NONE',  ( 5.551115123125764829E-17, 0.000000000000000000, -1.000000000000000000 ) ) ;
#173771=AXIS2_PLACEMENT_3D ( 'NONE', #170133, #82749, #54264 ) ;
#174420=ORIENTED_EDGE ( 'NONE', *, *, #57845, .T. ) ;
#174545=AXIS2_PLACEMENT_3D ( 'NONE', #72191, #121056, #188089 ) ;
#174590=VERTEX_POINT ( 'NONE', #182670 ) ;
#175042=DIRECTION ( 'NONE',  ( 0.000000000000000000, 1.000000000000000000, 0.000000000000000000 ) ) ;
#175064=ORIENTED_EDGE ( 'NONE', *, *, #194941, .F. ) ;
#175162=DIRECTION ( 'NONE',  ( -5.551115123125765446E-17, 0.000000000000000000, 1.000000000000000000 ) ) ;
#175363=ORIENTED_EDGE ( 'NONE', *, *, #190193, .T. ) ;
#175488=ORIENTED_EDGE ( 'NONE', *, *, #76548, .F. ) ;
#175554=FACE_OUTER_BOUND ( 'NONE', #50360, .T. ) ;
#175824=CIRCLE ( 'NONE', #144773, 2.500000000000007994 ) ;
#175904=DIRECTION ( 'NONE',  ( 5.551115123125764829E-17, 0.000000000000000000, -1.000000000000000000 ) ) ;
#176075=DIRECTION ( 'NONE',  ( 0.000000000000000000, 1.000000000000000000, 0.000000000000000000 ) ) ;
#176220=DIRECTION ( 'NONE',  ( -0.000000000000000000, -1.000000000000000000, -0.000000000000000000 ) ) ;
#176418=DIRECTION ( 'NONE',  ( -5.551115123125782702E-17, 0.000000000000000000, 1.000000000000000000 ) ) ;
#177194=ORIENTED_EDGE ( 'NONE', *, *, #26695, .T. ) ;
#177561=ORIENTED_EDGE ( 'NONE', *, *, #123084, .T. ) ;
#177684=CARTESIAN_POINT ( 'NONE',  ( -0.6170404364503375705, 3.466143782776612170, 1.902435570468860027 ) ) ;
#177763=AXIS2_PLACEMENT_3D ( 'NONE', #36609, #132029, #182860 ) ;
#178304=DIRECTION ( 'NONE',  ( 0.000000000000000000, -1.000000000000000000, 0.000000000000000000 ) ) ;
#178677=EDGE_CURVE ( 'NONE', #10457, #180001, #212080, .T. ) ;
#178733=AXIS2_PLACEMENT_3D ( 'NONE', #63808, #132055, #198066 ) ;
#178764=DIRECTION ( 'NONE',  ( 0.000000000000000000, 1.000000000000000000, 0.000000000000000000 ) ) ;
#179041=AXIS2_PLACEMENT_3D ( 'NONE', #152039, #3609, #69687 ) ;
#179373=AXIS2_PLACEMENT_3D ( 'NONE', #33234, #131850, #67830 ) ;
#179389=CARTESIAN_POINT ( 'NONE',  ( 1.124100812432970948E-16, 3.400000000000000355, -2.025000000000006573 ) ) ;
#179669=DIRECTION ( 'NONE',  ( 5.551115123125764213E-17, 0.000000000000000000, -1.000000000000000000 ) ) ;
#180001=VERTEX_POINT ( 'NONE', #210222 ) ;
#180152=DIRECTION ( 'NONE',  ( -5.551115123125758667E-17, 0.000000000000000000, 1.000000000000000000 ) ) ;
#180339=VECTOR ( 'NONE', #135246, 1000.000000000000000 ) ;
#180453=EDGE_CURVE ( 'NONE', #92739, #116046, #29351, .T. ) ;
#180514=ORIENTED_EDGE ( 'NONE', *, *, #181170, .F. ) ;
#181170=EDGE_CURVE ( 'NONE', #180001, #105092, #122835, .T. ) ;
#181245=EDGE_CURVE ( 'NONE', #174590, #140877, #36130, .T. ) ;
#181380=LINE ( 'NONE', #198676, #127991 ) ;
#181438=DIRECTION ( 'NONE',  ( 0.000000000000000000, 1.000000000000000000, 0.000000000000000000 ) ) ;
#181451=AXIS2_PLACEMENT_3D ( 'NONE', #84727, #19719, #105269 ) ;
#181464=AXIS2_PLACEMENT_3D ( 'NONE', #44293, #110415, #176418 ) ;
#181670=VERTEX_POINT ( 'NONE', #65360 ) ;
#182103=AXIS2_PLACEMENT_3D ( 'NONE', #202318, #122259, #120103 ) ;
#182303=ADVANCED_FACE ( 'NONE', ( #188736 ), #8603, .F. ) ;
#182433=DIRECTION ( 'NONE',  ( 2.935049515055183778E-17, -0.8987940462991643731, 0.4383711467890826219 ) ) ;
#182469=DIRECTION ( 'NONE',  ( 0.000000000000000000, -1.000000000000000000, 0.000000000000000000 ) ) ;
#182670=CARTESIAN_POINT ( 'NONE',  ( 1.673838217086941410E-16, 2.099999999999997868, 2.500000000000000000 ) ) ;
#182672=DIRECTION ( 'NONE',  ( -5.551115123125764829E-17, 0.000000000000000000, 1.000000000000000000 ) ) ;
#182678=VERTEX_POINT ( 'NONE', #107367 ) ;
#182738=ORIENTED_EDGE ( 'NONE', *, *, #43463, .F. ) ;
#182860=DIRECTION ( 'NONE',  ( -5.551115123125765446E-17, 0.000000000000000000, 1.000000000000000000 ) ) ;
#183591=ORIENTED_EDGE ( 'NONE', *, *, #194941, .T. ) ;
#183763=DIRECTION ( 'NONE',  ( 5.551115123125765446E-17, 0.000000000000000000, -1.000000000000000000 ) ) ;
#184068=TOROIDAL_SURFACE ( 'NONE', #204774, 1.600000000000000311, 0.1000000000000000056 ) ;
#184168=CIRCLE ( 'NONE', #97787, 0.09999999999999982514 ) ;
#184241=AXIS2_PLACEMENT_3D ( 'NONE', #57203, #173101, #9515 ) ;
#184302=CARTESIAN_POINT ( 'NONE',  ( -1.665334536937735057E-16, -0.5000000000000004441, 3.000000000000010214 ) ) ;
#184303=EDGE_LOOP ( 'NONE', ( #169297, #114874, #83957, #68241 ) ) ;
#184337=DIRECTION ( 'NONE',  ( 1.779758311459930245E-16, 0.000000000000000000, -1.000000000000000000 ) ) ;
#184348=ADVANCED_FACE ( 'NONE', ( #170715, #21234 ), #88412, .T. ) ;
#184764=VERTEX_POINT ( 'NONE', #204250 ) ;
#184897=VECTOR ( 'NONE', #106141, 1000.000000000000000 ) ;
#184931=ORIENTED_EDGE ( 'NONE', *, *, #165187, .F. ) ;
#185730=FACE_OUTER_BOUND ( 'NONE', #89622, .T. ) ;
#185826=ORIENTED_EDGE ( 'NONE', *, *, #97562, .F. ) ;
#185905=LINE ( 'NONE', #119930, #74357 ) ;
#186160=CARTESIAN_POINT ( 'NONE',  ( 1.004302930252164871E-16, 3.599999999999999201, 1.500000000000000222 ) ) ;
#186194=ORIENTED_EDGE ( 'NONE', *, *, #91960, .F. ) ;
#186296=EDGE_CURVE ( 'NONE', #147150, #201525, #188261, .T. ) ;
#186306=DIRECTION ( 'NONE',  ( -5.551115123125782702E-17, 0.000000000000000000, 1.000000000000000000 ) ) ;
#186717=DIRECTION ( 'NONE',  ( -5.551115123125765446E-17, 0.000000000000000000, 1.000000000000000000 ) ) ;
#186948=ORIENTED_EDGE ( 'NONE', *, *, #16428, .F. ) ;
#187209=FACE_OUTER_BOUND ( 'NONE', #71265, .T. ) ;
#187293=EDGE_CURVE ( 'NONE', #149924, #59046, #146863, .T. ) ;
#187388=CARTESIAN_POINT ( 'NONE',  ( 0.000000000000000000, 4.400000000000001243, 0.000000000000000000 ) ) ;
#187585=DIRECTION ( 'NONE',  ( 0.000000000000000000, -1.000000000000000000, 0.000000000000000000 ) ) ;
#187781=DIRECTION ( 'NONE',  ( -0.000000000000000000, -1.000000000000000000, -0.000000000000000000 ) ) ;
#187801=ADVANCED_FACE ( 'NONE', ( #134042 ), #51701, .F. ) ;
#188089=DIRECTION ( 'NONE',  ( 1.779758311459934189E-16, 0.000000000000000000, -1.000000000000000000 ) ) ;
#188223=EDGE_LOOP ( 'NONE', ( #80522, #129901 ) ) ;
#188252=CARTESIAN_POINT ( 'NONE',  ( -1.332267629550188046E-16, 4.000000000000003553, 2.400000000000007461 ) ) ;
#188254=TOROIDAL_SURFACE ( 'NONE', #177763, 2.149999999999999911, 0.1000000000000000056 ) ;
#188261=CIRCLE ( 'NONE', #181451, 2.650000000000008349 ) ;
#188447=ORIENTED_EDGE ( 'NONE', *, *, #86344, .T. ) ;
#188635=EDGE_CURVE ( 'NONE', #166237, #147669, #63700, .T. ) ;
#188681=CARTESIAN_POINT ( 'NONE',  ( 1.124100812432970948E-16, 3.500000000000003109, -2.025000000000006573 ) ) ;
#188736=FACE_OUTER_BOUND ( 'NONE', #15026, .T. ) ;
#189311=ADVANCED_FACE ( 'NONE', ( #50914 ), #98599, .F. ) ;
#189321=ORIENTED_EDGE ( 'NONE', *, *, #1852, .F. ) ;
#189468=LINE ( 'NONE', #91996, #184897 ) ;
#189709=CARTESIAN_POINT ( 'NONE',  ( 0.000000000000000000, 3.599999999999999201, 0.000000000000000000 ) ) ;
#189882=AXIS2_PLACEMENT_3D ( 'NONE', #109549, #208023, #13017 ) ;
#190193=EDGE_CURVE ( 'NONE', #116046, #92739, #57159, .T. ) ;
#190439=DIRECTION ( 'NONE',  ( -5.551115123125765446E-17, 0.000000000000000000, 1.000000000000000000 ) ) ;
#190530=EDGE_CURVE ( 'NONE', #191870, #29472, #37090, .T. ) ;
#190574=FACE_OUTER_BOUND ( 'NONE', #121523, .T. ) ;
#190877=EDGE_LOOP ( 'NONE', ( #159056, #75964 ) ) ;
#190974=CYLINDRICAL_SURFACE ( 'NONE', #33453, 2.250000000000006661 ) ;
#191322=AXIS2_PLACEMENT_3D ( 'NONE', #112023, #95728, #160700 ) ;
#191359=( NAMED_UNIT ( * ) PLANE_ANGLE_UNIT ( ) SI_UNIT ( $, .RADIAN. ) );
#191591=CARTESIAN_POINT ( 'NONE',  ( 5.339274934379788269E-16, -0.5000000000000004441, -3.000000000000000444 ) ) ;
#191686=DIRECTION ( 'NONE',  ( 5.551115123125764829E-17, 0.000000000000000000, -1.000000000000000000 ) ) ;
#191870=VERTEX_POINT ( 'NONE', #179389 ) ;
#192259=CIRCLE ( 'NONE', #102279, 1.600000000000005196 ) ;
#192313=FACE_OUTER_BOUND ( 'NONE', #79746, .T. ) ;
#192325=ORIENTED_EDGE ( 'NONE', *, *, #83669, .F. ) ;
#192833=CARTESIAN_POINT ( 'NONE',  ( 1.249000902703297164E-16, 4.400000000000001243, -2.250000000000000000 ) ) ;
#193064=CYLINDRICAL_SURFACE ( 'NONE', #193133, 1.500000000000005107 ) ;
#193133=AXIS2_PLACEMENT_3D ( 'NONE', #208241, #161660, #60943 ) ;
#193392=DIRECTION ( 'NONE',  ( -5.551115123125764829E-17, 0.000000000000000000, 1.000000000000000000 ) ) ;
#193559=ORIENTED_EDGE ( 'NONE', *, *, #131422, .T. ) ;
#194023=AXIS2_PLACEMENT_3D ( 'NONE', #84155, #2876, #5008 ) ;
#194213=VERTEX_POINT ( 'NONE', #157113 ) ;
#194547=EDGE_LOOP ( 'NONE', ( #175363, #207853 ) ) ;
#194649=DIRECTION ( 'NONE',  ( 0.000000000000000000, -1.000000000000000000, 0.000000000000000000 ) ) ;
#194789=DIRECTION ( 'NONE',  ( -1.000000000000000000, 0.000000000000000000, -5.551115123125765446E-17 ) ) ;
#194826=ADVANCED_BREP_SHAPE_REPRESENTATION ( '', ( #13191, #200407 ), #13801 ) ;
#194880=DIRECTION ( 'NONE',  ( -5.551115123125765446E-17, 0.000000000000000000, 1.000000000000000000 ) ) ;
#194941=EDGE_CURVE ( 'NONE', #194213, #202678, #171709, .T. ) ;
#195057=FACE_OUTER_BOUND ( 'NONE', #77913, .T. ) ;
#195070=CIRCLE ( 'NONE', #126042, 0.09999999999999982514 ) ;
#195087=VERTEX_POINT ( 'NONE', #53604 ) ;
#195250=ORIENTED_EDGE ( 'NONE', *, *, #78041, .T. ) ;
#195380=AXIS2_PLACEMENT_3D ( 'NONE', #213155, #194789, #47506 ) ;
#195749=CARTESIAN_POINT ( 'NONE',  ( 0.000000000000000000, 3.900000000000000799, 0.000000000000000000 ) ) ;
#195867=CARTESIAN_POINT ( 'NONE',  ( 1.526556658859585313E-16, 0.000000000000000000, -2.750000000000000000 ) ) ;
#196796=AXIS2_PLACEMENT_3D ( 'NONE', #149417, #165666, #33529 ) ;
#197110=CARTESIAN_POINT ( 'NONE',  ( 0.000000000000000000, 3.466143782776612170, 0.000000000000000000 ) ) ;
#197157=DIRECTION ( 'NONE',  ( 0.000000000000000000, -1.000000000000000000, 0.000000000000000000 ) ) ;
#197364=EDGE_LOOP ( 'NONE', ( #186948, #208045, #118345, #211853 ) ) ;
#197886=VERTEX_POINT ( 'NONE', #155909 ) ;
#197949=DIRECTION ( 'NONE',  ( -5.551115123125764829E-17, 0.000000000000000000, 1.000000000000000000 ) ) ;
#198066=DIRECTION ( 'NONE',  ( 5.551115123125764213E-17, 0.000000000000000000, -1.000000000000000000 ) ) ;
#198676=CARTESIAN_POINT ( 'NONE',  ( 1.274170411194398450E-16, 1.750000000000001554, 1.903066852858540603 ) ) ;
#198886=CARTESIAN_POINT ( 'NONE',  ( 1.124100812432970948E-16, 3.500000000000003109, -2.025000000000006573 ) ) ;
#198933=AXIS2_PLACEMENT_3D ( 'NONE', #125829, #9851, #73789 ) ;
#199292=DIRECTION ( 'NONE',  ( -5.551115123125764829E-17, 0.000000000000000000, 1.000000000000000000 ) ) ;
#199387=ORIENTED_EDGE ( 'NONE', *, *, #133578, .F. ) ;
#199417=CONICAL_SURFACE ( 'NONE', #81925, 2.000000000000006217, 0.01725463330310792257 ) ;
#199489=VECTOR ( 'NONE', #20387, 1000.000000000000114 ) ;
#199818=PRODUCT_DEFINITION_CONTEXT ( 'detailed design', #29814, 'design' ) ;
#199854=CARTESIAN_POINT ( 'NONE',  ( 1.673838217086941410E-16, 3.900000000000000799, 2.500000000000000000 ) ) ;
#200407=AXIS2_PLACEMENT_3D ( 'NONE', #95216, #132002, #161266 ) ;
#200849=EDGE_CURVE ( 'NONE', #182678, #106531, #19862, .T. ) ;
#200864=CIRCLE ( 'NONE', #152509, 2.250000000000006661 ) ;
#201050=CARTESIAN_POINT ( 'NONE',  ( 1.249000902703301108E-16, 4.500000000000003553, -2.250000000000006661 ) ) ;
#201525=VERTEX_POINT ( 'NONE', #68739 ) ;
#201857=CIRCLE ( 'NONE', #38915, 0.1000000000000000472 ) ;
#202315=EDGE_LOOP ( 'NONE', ( #159080, #122083, #106602, #48801 ) ) ;
#202318=CARTESIAN_POINT ( 'NONE',  ( 0.000000000000000000, 4.400000000000001243, 0.000000000000000000 ) ) ;
#202515=DIRECTION ( 'NONE',  ( -5.551115123125764829E-17, 0.000000000000000000, 1.000000000000000000 ) ) ;
#202594=ORIENTED_EDGE ( 'NONE', *, *, #109243, .F. ) ;
#202620=ORIENTED_EDGE ( 'NONE', *, *, #76548, .T. ) ;
#202649=AXIS2_PLACEMENT_3D ( 'NONE', #157923, #58272, #88648 ) ;
#202678=VERTEX_POINT ( 'NONE', #92280 ) ;
#202971=ORIENTED_EDGE ( 'NONE', *, *, #31468, .T. ) ;
#203727=MECHANICAL_DESIGN_GEOMETRIC_PRESENTATION_REPRESENTATION('',(#106870),#110431);
#203816=DIRECTION ( 'NONE',  ( 5.551115123125764213E-17, 0.000000000000000000, -1.000000000000000000 ) ) ;
#203949=CARTESIAN_POINT ( 'NONE',  ( 1.841222038795635206E-16, 0.000000000000000000, 2.750000000000000000 ) ) ;
#204010=CARTESIAN_POINT ( 'NONE',  ( 0.000000000000000000, 2.000000000000001776, 0.000000000000000000 ) ) ;
#204250=CARTESIAN_POINT ( 'NONE',  ( -1.665334536937729880E-16, -0.5000000000000004441, 3.000000000000000444 ) ) ;
#204774=AXIS2_PLACEMENT_3D ( 'NONE', #114870, #178764, #115933 ) ;
#204798=FACE_OUTER_BOUND ( 'NONE', #165922, .T. ) ;
#204906=EDGE_CURVE ( 'NONE', #34978, #106531, #2848, .T. ) ;
#205328=DIRECTION ( 'NONE',  ( 1.779758311459934189E-16, 0.000000000000000000, -1.000000000000000000 ) ) ;
#205697=DIRECTION ( 'NONE',  ( 5.551115123125764213E-17, 0.000000000000000000, -1.000000000000000000 ) ) ;
#205992=VERTEX_POINT ( 'NONE', #146895 ) ;
#206068=VECTOR ( 'NONE', #30646, 1000.000000000000114 ) ;
#206090=TOROIDAL_SURFACE ( 'NONE', #112788, 2.600000000000000089, 0.1000000000000000056 ) ;
#206267=EDGE_LOOP ( 'NONE', ( #39133, #49059, #12053, #11986 ) ) ;
#206340=VERTEX_POINT ( 'NONE', #199854 ) ;
#206348=ADVANCED_FACE ( 'NONE', ( #185730 ), #214025, .T. ) ;
#206431=ORIENTED_EDGE ( 'NONE', *, *, #21174, .T. ) ;
#206699=CIRCLE ( 'NONE', #113400, 2.750000000000008438 ) ;
#207131=EDGE_LOOP ( 'NONE', ( #161900, #96760, #19050, #167234 ) ) ;
#207184=FACE_OUTER_BOUND ( 'NONE', #140863, .T. ) ;
#207194=AXIS2_PLACEMENT_3D ( 'NONE', #115942, #20495, #86580 ) ;
#207372=DIRECTION ( 'NONE',  ( -5.551115123125766062E-17, 0.000000000000000000, 1.000000000000000000 ) ) ;
#207396=CARTESIAN_POINT ( 'NONE',  ( 0.000000000000000000, 2.099999999999997868, 0.000000000000000000 ) ) ;
#207618=( LENGTH_UNIT ( ) NAMED_UNIT ( * ) SI_UNIT ( .MILLI., .METRE. ) );
#207628=CARTESIAN_POINT ( 'NONE',  ( 0.000000000000000000, 2.000000000000001776, 0.000000000000000000 ) ) ;
#207670=EDGE_LOOP ( 'NONE', ( #192325, #121346 ) ) ;
#207777=ORIENTED_EDGE ( 'NONE', *, *, #31316, .T. ) ;
#207853=ORIENTED_EDGE ( 'NONE', *, *, #180453, .T. ) ;
#208023=DIRECTION ( 'NONE',  ( 0.000000000000000000, 1.000000000000000000, 0.000000000000000000 ) ) ;
#208045=ORIENTED_EDGE ( 'NONE', *, *, #34501, .T. ) ;
#208078=ORIENTED_EDGE ( 'NONE', *, *, #150919, .T. ) ;
#208241=CARTESIAN_POINT ( 'NONE',  ( 0.000000000000000000, 6.999999999999999112, 0.000000000000000000 ) ) ;
#208293=CIRCLE ( 'NONE', #146185, 2.000000000000006661 ) ;
#208508=CIRCLE ( 'NONE', #184241, 3.000000000000010214 ) ;
#208561=LINE ( 'NONE', #25558, #101898 ) ;
#208725=DIRECTION ( 'NONE',  ( 0.000000000000000000, -1.000000000000000000, 0.000000000000000000 ) ) ;
#209269=AXIS2_PLACEMENT_3D ( 'NONE', #151333, #152391, #23436 ) ;
#210185=ADVANCED_FACE ( 'NONE', ( #195057 ), #106647, .F. ) ;
#210222=CARTESIAN_POINT ( 'NONE',  ( 1.117161918529060416E-16, 3.466143782776612170, -2.000000000000000000 ) ) ;
#210329=ORIENTED_EDGE ( 'NONE', *, *, #147396, .F. ) ;
#210453=ORIENTED_EDGE ( 'NONE', *, *, #187293, .F. ) ;
#210722=EDGE_LOOP ( 'NONE', ( #50964, #108849 ) ) ;
#210742=DIRECTION ( 'NONE',  ( -5.551115123125766062E-17, 0.000000000000000000, 1.000000000000000000 ) ) ;
#211180=ORIENTED_EDGE ( 'NONE', *, *, #91960, .T. ) ;
#211272=EDGE_CURVE ( 'NONE', #29472, #78316, #113617, .T. ) ;
#211509=AXIS2_PLACEMENT_3D ( 'NONE', #32009, #181438, #210742 ) ;
#211853=ORIENTED_EDGE ( 'NONE', *, *, #136835, .F. ) ;
#212080=CIRCLE ( 'NONE', #125770, 2.000000000000006217 ) ;
#212318=CARTESIAN_POINT ( 'NONE',  ( 0.000000000000000000, 4.500000000000003553, 0.000000000000000000 ) ) ;
#212475=DIRECTION ( 'NONE',  ( -0.000000000000000000, -1.000000000000000000, -0.000000000000000000 ) ) ;
#212986=LINE ( 'NONE', #142716, #153433 ) ;
#212994=ADVANCED_FACE ( 'NONE', ( #61348 ), #75670, .F. ) ;
#213155=CARTESIAN_POINT ( 'NONE',  ( -1.304512053934558738E-16, 4.099999999999999645, 2.350000000000007194 ) ) ;
#213402=CIRCLE ( 'NONE', #165028, 2.600000000000008082 ) ;
#213612=ORIENTED_EDGE ( 'NONE', *, *, #187293, .T. ) ;
#214011=AXIS2_PLACEMENT_3D ( 'NONE', #30996, #159912, #160985 ) ;
#214025=TOROIDAL_SURFACE ( 'NONE', #99488, 2.400000000000000355, 0.1000000000000000056 ) ;
#214205=CIRCLE ( 'NONE', #17253, 2.000000000000006217 ) ;
#214224=EDGE_LOOP ( 'NONE', ( #64246, #64342, #111294, #158789 ) ) ;
ENDSEC;
END-ISO-10303-21;
